ISO-10303-21;
HEADER;
FILE_DESCRIPTION (('STEP AP214'),
    '1' );
FILE_NAME ('hex flange bolt small_iso_ISO 4162 - M5 x 40 x 16-N.step',
    '2026-10-25T07:12:54',
    ( '' ),
    ( '' ),
    'SwSTEP 2.0',
    'SolidWorks 2026',
    '' );
FILE_SCHEMA (( 'AUTOMOTIVE_DESIGN' ));
ENDSEC;

DATA;
#7=EDGE_LOOP ( 'NONE', ( #12409, #2488, #778, #882 ) ) ;
#8=EDGE_CURVE ( 'NONE', #8677, #8586, #7240, .T. ) ;
#50=ORIENTED_EDGE ( 'NONE', *, *, #11088, .F. ) ;
#55=CARTESIAN_POINT ( 'NONE',  ( 4.055492966679659084, -3.795017426214758682, 0.5629142681442622642 ) ) ;
#56=VECTOR ( 'NONE', #10401, 1000.000000000000114 ) ;
#65=VERTEX_POINT ( 'NONE', #4105 ) ;
#70=STYLED_ITEM('',(#13712),#1029);
#75=CARTESIAN_POINT ( 'NONE',  ( 4.052424581287595196, 3.786734753434853662, 0.5771415817955924954 ) ) ;
#78=ORIENTED_EDGE ( 'NONE', *, *, #4870, .T. ) ;
#84=CARTESIAN_POINT ( 'NONE',  ( 5.599999999999999645, 4.041451884327382338, 0.000000000000000000 ) ) ;
#87=CARTESIAN_POINT ( 'NONE',  ( 4.050880675075949178, 1.379097446046194220, 3.567934390854430760 ) ) ;
#105=CARTESIAN_POINT ( 'NONE',  ( 4.093692494532774617, 2.021783646005766322, -3.501831996793843160 ) ) ;
#121=B_SPLINE_CURVE_WITH_KNOTS ( 'NONE', 3,
 ( #11045, #8921, #1705, #7048, #10078, #9050 ),
 .UNSPECIFIED., .F., .F.,
 ( 4, 2, 4 ),
 ( 0.000000000000000000, 0.002086519881787260184, 0.004173039763574520368 ),
 .UNSPECIFIED. ) ;
#129=CYLINDRICAL_SURFACE ( 'NONE', #612, 2.500000000000000444 ) ;
#142=B_SPLINE_CURVE_WITH_KNOTS ( 'NONE', 3,
 ( #2843, #11275, #8032, #7064, #8173 ),
 .UNSPECIFIED., .F., .F.,
 ( 4, 1, 4 ),
 ( 0.000000000000000000, 0.002020725942163692675, 0.004041451884327385349 ),
 .UNSPECIFIED. ) ;
#184=CARTESIAN_POINT ( 'NONE',  ( 4.033901012035946643, -3.740908793664254883, 0.5205559028926849408 ) ) ;
#237=CARTESIAN_POINT ( 'NONE',  ( 4.050823680195223098, 2.400527758044901372, 2.978030508226146900 ) ) ;
#258=( BOUNDED_SURFACE ( )  B_SPLINE_SURFACE ( 3, 2, ( 
 ( #4456, #8885, #3626 ),
 ( #7848, #4733, #425 ),
 ( #12875, #2579, #6804 ),
 ( #11009, #4594, #5571 ),
 ( #1531, #5776, #3689 ),
 ( #9780, #6677, #7912 ) ),
 .UNSPECIFIED., .F., .F., .F. ) 
 B_SPLINE_SURFACE_WITH_KNOTS ( ( 4, 2, 4 ),
 ( 3, 3 ),
 ( 0.01651999345535506980, 0.01858032176739836394, 0.02064065007944165808 ),
 ( 0.000000000000000000, 1.000000000000000000 ),
 .UNSPECIFIED. ) 
 GEOMETRIC_REPRESENTATION_ITEM ( )  RATIONAL_B_SPLINE_SURFACE ( (
 ( 1.000000000000000000, 0.8047781103519393575, 1.000000000000000000),
 ( 1.000000000000000000, 0.8123785825603968558, 1.000000000000000000),
 ( 1.000000000000000000, 0.8190671539788806355, 1.000000000000000000),
 ( 1.000000000000000000, 0.8192352254834333047, 1.000000000000000000),
 ( 1.000000000000000000, 0.8126129677212012847, 1.000000000000000000),
 ( 1.000000000000000000, 0.8047712537969730073, 1.000000000000000000) ) ) 
 REPRESENTATION_ITEM ( '' )  SURFACE ( )  );
#274=CARTESIAN_POINT ( 'NONE',  ( 3.972066048304770725, 3.435565134476467275, 1.180968096049824556 ) ) ;
#296=CARTESIAN_POINT ( 'NONE',  ( 0.000000000000000000, 0.000000000000000000, 0.000000000000000000 ) ) ;
#308=FACE_OUTER_BOUND ( 'NONE', #7358, .T. ) ;
#315=CIRCLE ( 'NONE', #7843, 5.371010071662833063 ) ;
#341=EDGE_CURVE ( 'NONE', #7290, #12675, #5666, .T. ) ;
#356=CARTESIAN_POINT ( 'NONE',  ( 0.3126073911696407026, -2.020725942163686728, 3.500000000000000444 ) ) ;
#364=DIRECTION ( 'NONE',  ( 0.000000000000000000, 0.000000000000000000, -1.000000000000000000 ) ) ;
#370=LINE ( 'NONE', #9650, #12630 ) ;
#393=CARTESIAN_POINT ( 'NONE',  ( 0.02944718078426972890, -0.6813962075686093023, 3.500000000000000000 ) ) ;
#425=CARTESIAN_POINT ( 'NONE',  ( 4.055492966679490330, -2.385006769472456156, -3.005124364834284023 ) ) ;
#430=AXIS2_PLACEMENT_3D ( 'NONE', #5828, #10990, #3471 ) ;
#432=B_SPLINE_CURVE_WITH_KNOTS ( 'NONE', 3,
 ( #8361, #5121, #6237, #1776, #4000, #1847, #9330, #10495, #8225, #2893, #12497, #7046, #11256, #8155, #2966, #799 ),
 .UNSPECIFIED., .F., .F.,
 ( 4, 3, 3, 3, 3, 4 ),
 ( 0.000000000000000000, 3.315506744709148100E-05, 6.608280158698798419E-05, 0.0001026520855291344940, 0.0001376952025664800986, 0.0001398064759190609653 ),
 .UNSPECIFIED. ) ;
#434=CARTESIAN_POINT ( 'NONE',  ( 4.050536630291693641, -3.778525289263164222, -0.5912575323401421112 ) ) ;
#454=ADVANCED_FACE ( 'NONE', ( #10541 ), #10406, .F. ) ;
#465=CARTESIAN_POINT ( 'NONE',  ( 0.3126073911696451990, -4.041451884327386779, -1.834154111220703958E-17 ) ) ;
#472=ORIENTED_EDGE ( 'NONE', *, *, #2154, .T. ) ;
#492=FACE_OUTER_BOUND ( 'NONE', #11376, .T. ) ;
#510=PLANE ( 'NONE',  #8859 ) ;
#511=DIRECTION ( 'NONE',  ( -1.000000000000000000, -0.000000000000000000, 0.000000000000000000 ) ) ;
#523=ORIENTED_EDGE ( 'NONE', *, *, #8703, .T. ) ;
#541=CARTESIAN_POINT ( 'NONE',  ( 4.180345304246196214, 2.049116244671343345, -3.591763845239305919 ) ) ;
#547=DIRECTION ( 'NONE',  ( -1.000000000000000000, -0.000000000000000000, -0.000000000000000000 ) ) ;
#598=ORIENTED_EDGE ( 'NONE', *, *, #2180, .F. ) ;
#608=CONICAL_SURFACE ( 'NONE', #7932, 2.055000000000000160, 0.7853981633974400633 ) ;
#612=AXIS2_PLACEMENT_3D ( 'NONE', #3177, #12770, #2130 ) ;
#616=ORIENTED_EDGE ( 'NONE', *, *, #729, .F. ) ;
#634=EDGE_LOOP ( 'NONE', ( #3180, #8410, #6248, #1528, #779 ) ) ;
#649=CIRCLE ( 'NONE', #11718, 2.055000000000000160 ) ;
#652=CARTESIAN_POINT ( 'NONE',  ( 4.055498735588912496, -1.410041617600660491, 3.568038744583366118 ) ) ;
#667=ORIENTED_EDGE ( 'NONE', *, *, #4356, .F. ) ;
#707=ADVANCED_FACE ( 'NONE', ( #3417 ), #11910, .F. ) ;
#709=EDGE_LOOP ( 'NONE', ( #11053, #4698, #8961, #667, #5980, #11825 ) ) ;
#710=CARTESIAN_POINT ( 'NONE',  ( 0.000000000000000000, 0.000000000000000000, 0.000000000000000000 ) ) ;
#717=DIRECTION ( 'NONE',  ( 0.000000000000000000, 0.000000000000000000, -1.000000000000000000 ) ) ;
#722=ORIENTED_EDGE ( 'NONE', *, *, #11850, .F. ) ;
#729=EDGE_CURVE ( 'NONE', #12709, #1912, #7570, .T. ) ;
#736=CONICAL_SURFACE ( 'NONE', #7395, 5.371010071662833063, 1.221730476396037490 ) ;
#760=ORIENTED_EDGE ( 'NONE', *, *, #7579, .T. ) ;
#764=CARTESIAN_POINT ( 'NONE',  ( 4.071447262713887127, -2.020725942163686284, 3.500000000000000444 ) ) ;
#778=ORIENTED_EDGE ( 'NONE', *, *, #2180, .T. ) ;
#779=ORIENTED_EDGE ( 'NONE', *, *, #7051, .F. ) ;
#799=CARTESIAN_POINT ( 'NONE',  ( 4.175813232069147674, 2.061359961916367833, 3.570380186727398097 ) ) ;
#811=PLANE ( 'NONE',  #7708 ) ;
#841=EDGE_LOOP ( 'NONE', ( #7114, #472, #9760, #1503 ) ) ;
#854=FACE_OUTER_BOUND ( 'NONE', #10660, .T. ) ;
#866=CARTESIAN_POINT ( 'NONE',  ( 3.961557105776161158, -1.423285172354515016, 3.500000000000000444 ) ) ;
#880=ORIENTED_EDGE ( 'NONE', *, *, #8833, .F. ) ;
#882=ORIENTED_EDGE ( 'NONE', *, *, #6921, .F. ) ;
#884=DIRECTION ( 'NONE',  ( -0.000000000000000000, 0.000000000000000000, 1.000000000000000000 ) ) ;
#898=VERTEX_POINT ( 'NONE', #4729 ) ;
#917=DIRECTION ( 'NONE',  ( 1.000000000000000000, 0.000000000000000000, -0.000000000000000000 ) ) ;
#920=CARTESIAN_POINT ( 'NONE',  ( 0.000000000000000000, 0.000000000000000000, 0.000000000000000000 ) ) ;
#942=B_SPLINE_CURVE_WITH_KNOTS ( 'NONE', 3,
 ( #7432, #87, #10669, #977 ),
 .UNSPECIFIED., .F., .F.,
 ( 4, 4 ),
 ( 0.000000000000000000, 0.002080789711329271950 ),
 .UNSPECIFIED. ) ;
#977=CARTESIAN_POINT ( 'NONE',  ( 3.973110223767137850, 2.263269463293572928E-11, 3.565797985667434222 ) ) ;
#984=DIRECTION ( 'NONE',  ( 1.000000000000000000, 0.000000000000000000, -0.000000000000000000 ) ) ;
#993=SURFACE_STYLE_USAGE ( .BOTH. , #2878 ) ;
#1029=MANIFOLD_SOLID_BREP ( 'FlangeHexFillet', #6053 ) ;
#1037=FACE_OUTER_BOUND ( 'NONE', #7504, .T. ) ;
#1038=DIRECTION ( 'NONE',  ( 1.000000000000000000, 0.000000000000000000, -0.000000000000000000 ) ) ;
#1053=DIRECTION ( 'NONE',  ( 0.000000000000000000, 0.000000000000000000, 1.000000000000000000 ) ) ;
#1054=( BOUNDED_SURFACE ( )  B_SPLINE_SURFACE ( 3, 2, ( 
 ( #13175, #7879, #5809 ),
 ( #3788, #1423, #2608 ),
 ( #5738, #10904, #3716 ),
 ( #9044, #2539, #11041 ),
 ( #4629, #5670, #10145 ),
 ( #9939, #5945, #10004 ) ),
 .UNSPECIFIED., .F., .F., .F. ) 
 B_SPLINE_SURFACE_WITH_KNOTS ( ( 4, 2, 4 ),
 ( 3, 3 ),
 ( 0.01652267773200353021, 0.01858309280828997212, 0.02064350788457641403 ),
 ( 0.000000000000000000, 1.000000000000000000 ),
 .UNSPECIFIED. ) 
 GEOMETRIC_REPRESENTATION_ITEM ( )  RATIONAL_B_SPLINE_SURFACE ( (
 ( 1.000000000000000000, 0.8047780975688292315, 1.000000000000000000),
 ( 1.000000000000000000, 0.8123789546324570177, 1.000000000000000000),
 ( 1.000000000000000000, 0.8190677982988761041, 1.000000000000000000),
 ( 1.000000000000000000, 0.8192346069552172150, 1.000000000000000000),
 ( 1.000000000000000000, 0.8126126759768884655, 1.000000000000000000),
 ( 1.000000000000000000, 0.8047712639311999094, 1.000000000000000000) ) ) 
 REPRESENTATION_ITEM ( '' )  SURFACE ( )  );
#1070=CARTESIAN_POINT ( 'NONE',  ( 4.030867648406620596, -2.329326259789657350, 2.965488570640411492 ) ) ;
#1083=DIRECTION ( 'NONE',  ( 0.000000000000000000, 0.000000000000000000, 1.000000000000000000 ) ) ;
#1094=CARTESIAN_POINT ( 'NONE',  ( 4.055492966679600464, 2.385006769472780785, 3.005124364834443451 ) ) ;
#1129=CARTESIAN_POINT ( 'NONE',  ( 0.000000000000000000, 3.061616997868383634E-16, -2.500000000000000444 ) ) ;
#1142=CARTESIAN_POINT ( 'NONE',  ( 4.175075985190098038, 4.120741555260245548, 3.964526709274768569E-16 ) ) ;
#1144=DIRECTION ( 'NONE',  ( 0.000000000000000000, 0.000000000000000000, 1.000000000000000000 ) ) ;
#1174=DIRECTION ( 'NONE',  ( 1.000000000000000000, 0.000000000000000000, 0.000000000000000000 ) ) ;
#1176=FACE_OUTER_BOUND ( 'NONE', #1752, .T. ) ;
#1191=CARTESIAN_POINT ( 'NONE',  ( -2.852594293689151105E-15, 3.375361811986501426, -1.153701847711632311 ) ) ;
#1212=CARTESIAN_POINT ( 'NONE',  ( 4.165266963751722784, 4.099263933823986683, 2.067493599750144616E-15 ) ) ;
#1224=DIRECTION ( 'NONE',  ( -1.000000000000000000, -0.000000000000000000, -0.000000000000000000 ) ) ;
#1235=EDGE_LOOP ( 'NONE', ( #3787, #8273, #4869 ) ) ;
#1252=CARTESIAN_POINT ( 'NONE',  ( 4.175572532730929431, 2.061029303918044064, -3.569807470274393602 ) ) ;
#1268=ORIENTED_EDGE ( 'NONE', *, *, #11850, .T. ) ;
#1276=B_SPLINE_CURVE_WITH_KNOTS ( 'NONE', 3,
 ( #9913, #434, #12128, #2653, #4667, #8890 ),
 .UNSPECIFIED., .F., .F.,
 ( 4, 2, 4 ),
 ( 9.961792871202292917E-20, 0.002086519881787258883, 0.004173039763574517766 ),
 .UNSPECIFIED. ) ;
#1278=VECTOR ( 'NONE', #10202, 1000.000000000000000 ) ;
#1286=( GEOMETRIC_REPRESENTATION_CONTEXT ( 3 ) GLOBAL_UNCERTAINTY_ASSIGNED_CONTEXT ( ( #9793 ) ) GLOBAL_UNIT_ASSIGNED_CONTEXT ( ( #8209, #4056, #2043 ) ) REPRESENTATION_CONTEXT ( 'NONE', 'WORKASPACE' ) );
#1329=DIRECTION ( 'NONE',  ( 0.000000000000000000, 0.000000000000000000, 1.000000000000000000 ) ) ;
#1359=CARTESIAN_POINT ( 'NONE',  ( 3.806834918298646731, 3.031088913245537864, 1.750000000000000666 ) ) ;
#1366=PLANE ( 'NONE',  #3601 ) ;
#1368=AXIS2_PLACEMENT_3D ( 'NONE', #11641, #2226, #6470 ) ;
#1372=ORIENTED_EDGE ( 'NONE', *, *, #11964, .F. ) ;
#1381=PLANE ( 'NONE',  #4015 ) ;
#1423=CARTESIAN_POINT ( 'NONE',  ( 4.033895293471413623, 1.419609371826631827, -3.500000000000000000 ) ) ;
#1425=CARTESIAN_POINT ( 'NONE',  ( 6.897297840755645792E-16, -2.686816014504582739, -2.346298152288354366 ) ) ;
#1449=B_SPLINE_CURVE_WITH_KNOTS ( 'NONE', 3,
 ( #4192, #1252, #3155, #8415, #7382, #12810, #8611, #8480, #12620, #4386, #8546, #7445, #3223, #105, #6416, #6289 ),
 .UNSPECIFIED., .F., .F.,
 ( 4, 3, 3, 3, 3, 4 ),
 ( -2.111273352581767125E-06, 0.000000000000000000, 3.519286887793215919E-05, 7.191842652067064129E-05, 0.0001049868727093590168, 0.0001382836236822123786 ),
 .UNSPECIFIED. ) ;
#1451=FACE_OUTER_BOUND ( 'NONE', #12593, .T. ) ;
#1455=ORIENTED_EDGE ( 'NONE', *, *, #12136, .F. ) ;
#1479=CARTESIAN_POINT ( 'NONE',  ( 4.114405500665260895, -2.025575754679711071, 3.508400121684938089 ) ) ;
#1503=ORIENTED_EDGE ( 'NONE', *, *, #11929, .F. ) ;
#1506=ORIENTED_EDGE ( 'NONE', *, *, #8296, .T. ) ;
#1522=CARTESIAN_POINT ( 'NONE',  ( 5.599999999999999645, -4.041451884327386779, 0.000000000000000000 ) ) ;
#1528=ORIENTED_EDGE ( 'NONE', *, *, #7291, .F. ) ;
#1531=CARTESIAN_POINT ( 'NONE',  ( 3.958484000407238579, -3.734437307742088485, -0.5317648453099828032 ) ) ;
#1581=CARTESIAN_POINT ( 'NONE',  ( 4.052424581287787042, 2.393186648133419414, -2.990837702970412959 ) ) ;
#1615=DIRECTION ( 'NONE',  ( 0.3420201433256622736, 1.150791560227853228E-16, 0.9396926207859106484 ) ) ;
#1617=DIRECTION ( 'NONE',  ( 0.000000000000000000, 0.000000000000000000, -1.000000000000000000 ) ) ;
#1623=CARTESIAN_POINT ( 'NONE',  ( 3.951447005078450925, 3.704664227300100254, -0.5833333333333329263 ) ) ;
#1640=ADVANCED_FACE ( 'NONE', ( #5191 ), #6734, .T. ) ;
#1644=ORIENTED_EDGE ( 'NONE', *, *, #4617, .F. ) ;
#1652=CARTESIAN_POINT ( 'NONE',  ( 4.086376042167605860, 1.979461949354204719, -3.571471332069177773 ) ) ;
#1689=EDGE_CURVE ( 'NONE', #2696, #1895, #4289, .T. ) ;
#1694=DIRECTION ( 'NONE',  ( -1.000000000000000000, -0.000000000000000000, 0.000000000000000000 ) ) ;
#1705=CARTESIAN_POINT ( 'NONE',  ( 3.972709601346591235, 2.746729940827189242, -2.374099244652734697 ) ) ;
#1722=CARTESIAN_POINT ( 'NONE',  ( 5.599999999999999645, -2.020725942163686284, 3.500000000000000444 ) ) ;
#1744=CARTESIAN_POINT ( 'NONE',  ( -1.372193374551966155E-15, -2.859595677584338969, 2.047034997319577609 ) ) ;
#1752=EDGE_LOOP ( 'NONE', ( #12756, #3736 ) ) ;
#1771=ORIENTED_EDGE ( 'NONE', *, *, #4489, .F. ) ;
#1773=CARTESIAN_POINT ( 'NONE',  ( 3.878089031707363521, 0.7015470581914173831, 3.500000000000000444 ) ) ;
#1776=CARTESIAN_POINT ( 'NONE',  ( 4.104070371397480876, 2.023683613428366002, 3.505122836902507810 ) ) ;
#1791=DIRECTION ( 'NONE',  ( 1.000000000000000000, 0.000000000000000000, -0.000000000000000000 ) ) ;
#1802=AXIS2_PLACEMENT_3D ( 'NONE', #8195, #12264, #11369 ) ;
#1804=AXIS2_PLACEMENT_3D ( 'NONE', #9785, #7582, #1329 ) ;
#1847=CARTESIAN_POINT ( 'NONE',  ( 4.124214193018069352, 2.028338413290941222, 3.513185186763553514 ) ) ;
#1848=CARTESIAN_POINT ( 'NONE',  ( 4.050536630291690088, -2.401306687817039265, 2.976670123173768445 ) ) ;
#1874=CARTESIAN_POINT ( 'NONE',  ( 3.951447005078451813, -1.347150628109131443, -3.500000000000000444 ) ) ;
#1886=SHAPE_DEFINITION_REPRESENTATION ( #13143, #5848 ) ;
#1890=CARTESIAN_POINT ( 'NONE',  ( 4.175813232069146785, -2.061359961916366057, 3.570380186727398542 ) ) ;
#1895=VERTEX_POINT ( 'NONE', #7597 ) ;
#1906=( LENGTH_UNIT ( ) NAMED_UNIT ( * ) SI_UNIT ( .MILLI., .METRE. ) );
#1912=VERTEX_POINT ( 'NONE', #8629 ) ;
#1914=B_SPLINE_CURVE_WITH_KNOTS ( 'NONE', 3,
 ( #4422, #9543, #1359, #12843, #11880 ),
 .UNSPECIFIED., .F., .F.,
 ( 4, 1, 4 ),
 ( 0.000000000000000000, 0.002020725942163690940, 0.004041451884327382747 ),
 .UNSPECIFIED. ) ;
#1920=CARTESIAN_POINT ( 'NONE',  ( 3.973110223767137850, 2.263269463293572928E-11, 3.565797985667434222 ) ) ;
#1929=DIRECTION ( 'NONE',  ( 0.000000000000000000, 0.000000000000000000, 1.000000000000000000 ) ) ;
#1964=DIRECTION ( 'NONE',  ( -1.000000000000000000, -0.000000000000000000, -0.000000000000000000 ) ) ;
#2004=CARTESIAN_POINT ( 'NONE',  ( 5.599999999999999645, 2.020725942163686284, -3.499999999999999556 ) ) ;
#2016=ORIENTED_EDGE ( 'NONE', *, *, #10894, .F. ) ;
#2018=VERTEX_POINT ( 'NONE', #5728 ) ;
#2019=ADVANCED_FACE ( 'NONE', ( #9864 ), #6886, .T. ) ;
#2031=CARTESIAN_POINT ( 'NONE',  ( 4.033901012036086087, 3.740908793663944021, -0.5205559028925770271 ) ) ;
#2043=( NAMED_UNIT ( * ) SI_UNIT ( $, .STERADIAN. ) SOLID_ANGLE_UNIT ( ) );
#2082=ORIENTED_EDGE ( 'NONE', *, *, #10013, .T. ) ;
#2095=CARTESIAN_POINT ( 'NONE',  ( 3.948103430091020272, 2.682758828852976229, -2.353325403973173024 ) ) ;
#2103=CARTESIAN_POINT ( 'NONE',  ( 0.3126073911696427010, 4.041451884327382338, -6.521455134176256610E-17 ) ) ;
#2120=CARTESIAN_POINT ( 'NONE',  ( 3.878096787214416530, -2.680238624820946214, 2.357690525401583415 ) ) ;
#2130=DIRECTION ( 'NONE',  ( 0.000000000000000000, 0.000000000000000000, 1.000000000000000000 ) ) ;
#2139=EDGE_CURVE ( 'NONE', #13432, #2696, #4430, .T. ) ;
#2142=CARTESIAN_POINT ( 'NONE',  ( 4.165266963751724560, -4.099263933823990236, 4.401844587977598791E-16 ) ) ;
#2154=EDGE_CURVE ( 'NONE', #13341, #13443, #7780, .T. ) ;
#2159=FACE_OUTER_BOUND ( 'NONE', #4630, .T. ) ;
#2180=EDGE_CURVE ( 'NONE', #10373, #4052, #370, .T. ) ;
#2187=MECHANICAL_DESIGN_GEOMETRIC_PRESENTATION_REPRESENTATION('',(#4406),#1286);
#2198=ORIENTED_EDGE ( 'NONE', *, *, #11069, .F. ) ;
#2200=LINE ( 'NONE', #3522, #6526 ) ;
#2207=CARTESIAN_POINT ( 'NONE',  ( 4.180345304246197990, 4.135116856707394817, -0.02129519942689619277 ) ) ;
#2226=DIRECTION ( 'NONE',  ( 1.000000000000000000, 0.000000000000000000, 0.000000000000000000 ) ) ;
#2236=AXIS2_PLACEMENT_3D ( 'NONE', #9076, #547, #4862 ) ;
#2245=DIRECTION ( 'NONE',  ( 0.000000000000000000, 1.000000000000000000, -1.073081856240829552E-16 ) ) ;
#2252=CARTESIAN_POINT ( 'NONE',  ( 3.948103430090711630, -2.682758828852738642, 2.353325403972896357 ) ) ;
#2258=CARTESIAN_POINT ( 'NONE',  ( 0.3126073911696399255, 2.020725942163686284, -3.499999999999999556 ) ) ;
#2268=( GEOMETRIC_REPRESENTATION_CONTEXT ( 3 ) GLOBAL_UNCERTAINTY_ASSIGNED_CONTEXT ( ( #7859 ) ) GLOBAL_UNIT_ASSIGNED_CONTEXT ( ( #1906, #3270, #9695 ) ) REPRESENTATION_CONTEXT ( 'NONE', 'WORKASPACE' ) );
#2271=( BOUNDED_SURFACE ( )  B_SPLINE_SURFACE ( 3, 2, ( 
 ( #7306, #11514, #13632 ),
 ( #4181, #2031, #8404 ),
 ( #12609, #3142, #7372 ),
 ( #11581, #2095, #2842 ),
 ( #12443, #7207, #1581 ),
 ( #1652, #11274, #541 ) ),
 .UNSPECIFIED., .F., .F., .F. ) 
 B_SPLINE_SURFACE_WITH_KNOTS ( ( 4, 2, 4 ),
 ( 3, 3 ),
 ( 0.01651999345535503164, 0.01858032176739832925, 0.02064065007944162339 ),
 ( 0.000000000000000000, 1.000000000000000000 ),
 .UNSPECIFIED. ) 
 GEOMETRIC_REPRESENTATION_ITEM ( )  RATIONAL_B_SPLINE_SURFACE ( (
 ( 1.000000000000000000, 0.8047781103519391355, 1.000000000000000000),
 ( 1.000000000000000000, 0.8123785825612301892, 1.000000000000000000),
 ( 1.000000000000000000, 0.8190671539777686361, 1.000000000000000000),
 ( 1.000000000000000000, 0.8192352254845479687, 1.000000000000000000),
 ( 1.000000000000000000, 0.8126129677203643986, 1.000000000000000000),
 ( 1.000000000000000000, 0.8047712537969725632, 1.000000000000000000) ) ) 
 REPRESENTATION_ITEM ( '' )  SURFACE ( )  );
#2273=CARTESIAN_POINT ( 'NONE',  ( 3.880206590543030742, 2.665671387532550618, 2.382921720510995822 ) ) ;
#2283=CARTESIAN_POINT ( 'NONE',  ( 3.973110223765528026, -0.6902454861566464928, 3.565797985667392034 ) ) ;
#2299=ORIENTED_EDGE ( 'NONE', *, *, #6921, .T. ) ;
#2317=ORIENTED_EDGE ( 'NONE', *, *, #5140, .F. ) ;
#2321=CARTESIAN_POINT ( 'NONE',  ( 4.114405500665256454, 4.051151509359430136, -5.737475420082528345E-17 ) ) ;
#2323=CARTESIAN_POINT ( 'NONE',  ( 4.158806965674310518, -4.075748668183988066, -0.05940377217583901054 ) ) ;
#2327=EDGE_CURVE ( 'NONE', #9556, #2018, #7651, .T. ) ;
#2364=DIRECTION ( 'NONE',  ( -0.000000000000000000, 0.000000000000000000, -1.000000000000000000 ) ) ;
#2376=DIRECTION ( 'NONE',  ( -1.000000000000000000, -0.000000000000000000, -0.000000000000000000 ) ) ;
#2396=DIRECTION ( 'NONE',  ( 1.000000000000000000, 0.000000000000000000, -0.000000000000000000 ) ) ;
#2439=CARTESIAN_POINT ( 'NONE',  ( 4.050536630291690976, 3.778525289263159781, 0.5912575323401418892 ) ) ;
#2453=DIRECTION ( 'NONE',  ( -1.000000000000000000, -0.000000000000000000, -0.000000000000000000 ) ) ;
#2455=FACE_OUTER_BOUND ( 'NONE', #12631, .T. ) ;
#2481=EDGE_CURVE ( 'NONE', #1895, #898, #1276, .T. ) ;
#2488=ORIENTED_EDGE ( 'NONE', *, *, #8643, .T. ) ;
#2515=DIRECTION ( 'NONE',  ( 0.000000000000000000, 0.000000000000000000, -1.000000000000000000 ) ) ;
#2539=CARTESIAN_POINT ( 'NONE',  ( 3.948111298835276894, -0.6968132764964354298, -3.500000000000154987 ) ) ;
#2579=CARTESIAN_POINT ( 'NONE',  ( 3.950241966888156320, -2.668221755853644073, -2.378504353000863158 ) ) ;
#2593=CARTESIAN_POINT ( 'NONE',  ( 0.000000000000000000, -3.031088913245534755, -1.750000000000001332 ) ) ;
#2608=CARTESIAN_POINT ( 'NONE',  ( 4.055487192203242941, 1.409979666030558354, -3.568038521265956664 ) ) ;
#2609=ORIENTED_EDGE ( 'NONE', *, *, #5768, .F. ) ;
#2629=COLOUR_RGB ( '',1.000000000000000000, 0.9490196078431372140, 0.9098039215686274384 ) ;
#2653=CARTESIAN_POINT ( 'NONE',  ( 3.973514160553462737, -2.741076955031366502, -2.383932505289870551 ) ) ;
#2674=CIRCLE ( 'NONE', #6872, 2.055000000000000160 ) ;
#2687=CARTESIAN_POINT ( 'NONE',  ( -2.837560373301905643E-16, 0.3423821193871246504, -3.499999999999999556 ) ) ;
#2692=VECTOR ( 'NONE', #2911, 1000.000000000000000 ) ;
#2696=VERTEX_POINT ( 'NONE', #1890 ) ;
#2715=ORIENTED_EDGE ( 'NONE', *, *, #9266, .F. ) ;
#2734=CARTESIAN_POINT ( 'NONE',  ( 5.100000000000002309, 0.000000000000000000, 5.200000000000001066 ) ) ;
#2740=CARTESIAN_POINT ( 'NONE',  ( 4.124214193018075569, -2.028338413290941666, 3.513185186763556622 ) ) ;
#2753=EDGE_LOOP ( 'NONE', ( #2317, #1268, #13413, #2609, #10383 ) ) ;
#2765=B_SPLINE_CURVE_WITH_KNOTS ( 'NONE', 3,
 ( #8853, #4492, #13050, #7612, #3595, #465 ),
 .UNSPECIFIED., .F., .F.,
 ( 4, 2, 4 ),
 ( 0.002044882221487524104, 0.003063384235218490244, 0.004081886248949456383 ),
 .UNSPECIFIED. ) ;
#2769=ORIENTED_EDGE ( 'NONE', *, *, #12174, .F. ) ;
#2797=CARTESIAN_POINT ( 'NONE',  ( 0.000000000000000000, -3.031088913245531202, 1.750000000000006439 ) ) ;
#2808=CARTESIAN_POINT ( 'NONE',  ( 4.132952817037859106, -2.031684012687264396, -3.518979934899745032 ) ) ;
#2825=CARTESIAN_POINT ( 'NONE',  ( 0.2174200650117528444, 2.185595227304856891, -3.214438021527932676 ) ) ;
#2839=CARTESIAN_POINT ( 'NONE',  ( 45.60000000000000142, 0.000000000000000000, 0.000000000000000000 ) ) ;
#2842=CARTESIAN_POINT ( 'NONE',  ( 3.972066048304756514, 2.740530939476224059, -2.384802634787894338 ) ) ;
#2843=CARTESIAN_POINT ( 'NONE',  ( 4.071447262713890680, -4.041451884327386779, 0.000000000000000000 ) ) ;
#2852=ORIENTED_EDGE ( 'NONE', *, *, #10894, .T. ) ;
#2856=ORIENTED_EDGE ( 'NONE', *, *, #8833, .T. ) ;
#2874=CARTESIAN_POINT ( 'NONE',  ( 4.158413352280807551, -2.044871626972826650, -3.541821552872960410 ) ) ;
#2878=SURFACE_SIDE_STYLE ('',( #9244 ) ) ;
#2892=ORIENTED_EDGE ( 'NONE', *, *, #8641, .F. ) ;
#2893=CARTESIAN_POINT ( 'NONE',  ( 4.158413352280808439, 2.044871626972822209, 3.541821552872961298 ) ) ;
#2911=DIRECTION ( 'NONE',  ( -1.000000000000000000, -0.000000000000000000, -0.000000000000000000 ) ) ;
#2920=CARTESIAN_POINT ( 'NONE',  ( 3.951447005078448260, 1.347150628109122339, -3.499999999999999112 ) ) ;
#2924=ADVANCED_FACE ( 'NONE', ( #2159 ), #2932, .T. ) ;
#2928=CARTESIAN_POINT ( 'NONE',  ( 0.000000000000000000, -3.031088913245531202, 1.750000000000006439 ) ) ;
#2932=CONICAL_SURFACE ( 'NONE', #1368, 5.371010071662833063, 1.221730476396037490 ) ;
#2947=CARTESIAN_POINT ( 'NONE',  ( 4.142654963991852846, -2.035398498734352746, -3.525413613457307971 ) ) ;
#2966=CARTESIAN_POINT ( 'NONE',  ( 4.175572532730931208, 2.061029303918050726, 3.569807470274392713 ) ) ;
#2994=ORIENTED_EDGE ( 'NONE', *, *, #8052, .T. ) ;
#2997=CARTESIAN_POINT ( 'NONE',  ( -1.438549683741723797E-15, -3.375361811986503202, 1.153701847711634532 ) ) ;
#3009=CARTESIAN_POINT ( 'NONE',  ( 0.000000000000000000, 0.000000000000000000, 0.000000000000000000 ) ) ;
#3010=ORIENTED_EDGE ( 'NONE', *, *, #1689, .T. ) ;
#3070=DIRECTION ( 'NONE',  ( -1.000000000000000000, -0.000000000000000000, -0.000000000000000000 ) ) ;
#3131=CARTESIAN_POINT ( 'NONE',  ( 4.071447262713887127, 2.020725942163686284, -3.499999999999999556 ) ) ;
#3138=B_SPLINE_CURVE_WITH_KNOTS ( 'NONE', 3,
 ( #3305, #3439, #5395, #6561 ),
 .UNSPECIFIED., .F., .F.,
 ( 4, 4 ),
 ( 0.000000000000000000, 0.002080789711329296236 ),
 .UNSPECIFIED. ) ;
#3142=CARTESIAN_POINT ( 'NONE',  ( 3.950241966887845457, 3.393956070637746514, -1.121495646998088569 ) ) ;
#3145=DIRECTION ( 'NONE',  ( 0.000000000000000000, 0.000000000000000000, 1.000000000000000000 ) ) ;
#3155=CARTESIAN_POINT ( 'NONE',  ( 4.175326769692854434, 2.060699556488891027, -3.569236330973487803 ) ) ;
#3156=PRESENTATION_STYLE_ASSIGNMENT (( #993 ) ) ;
#3160=CARTESIAN_POINT ( 'NONE',  ( 0.02944718078674397194, -0.6813962075909725247, -3.500000000000000000 ) ) ;
#3165=VERTEX_POINT ( 'NONE', #9420 ) ;
#3173=DIRECTION ( 'NONE',  ( 0.000000000000000000, 0.000000000000000000, 1.000000000000000000 ) ) ;
#3177=CARTESIAN_POINT ( 'NONE',  ( 0.000000000000000000, 0.000000000000000000, 0.000000000000000000 ) ) ;
#3180=ORIENTED_EDGE ( 'NONE', *, *, #11088, .T. ) ;
#3192=CARTESIAN_POINT ( 'NONE',  ( 4.175813232069150338, -4.122719923832746325, 2.362127131240695889E-16 ) ) ;
#3212=VECTOR ( 'NONE', #10478, 1000.000000000000000 ) ;
#3223=CARTESIAN_POINT ( 'NONE',  ( 4.104070371397485317, 2.023683613428364225, -3.505122836902508698 ) ) ;
#3251=EDGE_CURVE ( 'NONE', #13462, #12709, #10005, .T. ) ;
#3260=CARTESIAN_POINT ( 'NONE',  ( 3.961551342853837809, 2.319461885623310682, 2.982574167880912341 ) ) ;
#3270=( NAMED_UNIT ( * ) PLANE_ANGLE_UNIT ( ) SI_UNIT ( $, .RADIAN. ) );
#3295=DIRECTION ( 'NONE',  ( 0.000000000000000000, -1.073081856240829552E-16, -1.000000000000000000 ) ) ;
#3305=CARTESIAN_POINT ( 'NONE',  ( 4.175813232069148562, -2.061359961916374051, -3.570380186727397653 ) ) ;
#3316=ADVANCED_FACE ( 'NONE', ( #3326 ), #8315, .F. ) ;
#3322=CARTESIAN_POINT ( 'NONE',  ( 45.60000000000000142, 0.000000000000000000, 0.000000000000000000 ) ) ;
#3326=FACE_OUTER_BOUND ( 'NONE', #6919, .T. ) ;
#3335=CARTESIAN_POINT ( 'NONE',  ( 4.050480423730737911, -1.376911654797406070, 3.567926555162024282 ) ) ;
#3365=ORIENTED_EDGE ( 'NONE', *, *, #7224, .T. ) ;
#3417=FACE_OUTER_BOUND ( 'NONE', #709, .T. ) ;
#3430=EDGE_CURVE ( 'NONE', #1895, #4695, #13136, .T. ) ;
#3439=CARTESIAN_POINT ( 'NONE',  ( 4.050880675075948290, -1.379097446046192665, -3.567934390854430315 ) ) ;
#3471=DIRECTION ( 'NONE',  ( 1.000000000000000000, 0.000000000000000000, 0.000000000000000000 ) ) ;
#3482=DIRECTION ( 'NONE',  ( -1.000000000000000000, -0.000000000000000000, -0.000000000000000000 ) ) ;
#3504=DIRECTION ( 'NONE',  ( -0.000000000000000000, 0.000000000000000000, 1.000000000000000000 ) ) ;
#3522=CARTESIAN_POINT ( 'NONE',  ( 5.599999999999999645, 4.041451884327382338, 0.000000000000000000 ) ) ;
#3530=FACE_OUTER_BOUND ( 'NONE', #8948, .T. ) ;
#3561=DIRECTION ( 'NONE',  ( -1.000000000000000000, -0.000000000000000000, -0.000000000000000000 ) ) ;
#3563=EDGE_CURVE ( 'NONE', #10405, #5442, #4049, .T. ) ;
#3571=ADVANCED_FACE ( 'NONE', ( #3530 ), #1366, .F. ) ;
#3578=CARTESIAN_POINT ( 'NONE',  ( 4.151274195509685683, -2.039912954708743786, 3.533232880573501156 ) ) ;
#3586=VERTEX_POINT ( 'NONE', #7821 ) ;
#3591=CARTESIAN_POINT ( 'NONE',  ( 0.000000000000000000, -3.031088913245534755, -1.750000000000001332 ) ) ;
#3595=CARTESIAN_POINT ( 'NONE',  ( 0.2174200650117580902, -3.876582599186216616, -0.2855619784720681564 ) ) ;
#3598=DIRECTION ( 'NONE',  ( 0.000000000000000000, -0.8660254037844380415, 0.5000000000000012212 ) ) ;
#3601=AXIS2_PLACEMENT_3D ( 'NONE', #5611, #3598, #6718 ) ;
#3626=CARTESIAN_POINT ( 'NONE',  ( 4.180231891692620216, -2.049421325483211653, -3.591231015387276848 ) ) ;
#3655=FACE_OUTER_BOUND ( 'NONE', #5996, .T. ) ;
#3662=PRODUCT ( 'hex flange bolt small_iso_ISO 4162 - M5 x 40 x 16-N', 'hex flange bolt small_iso_ISO 4162 - M5 x 40 x 16-N', '', ( #8053 ) ) ;
#3689=CARTESIAN_POINT ( 'NONE',  ( 4.052424581287701777, -3.786734753435149425, -0.5771415817957858962 ) ) ;
#3710=CARTESIAN_POINT ( 'NONE',  ( 5.599999999999999645, 0.000000000000000000, 0.000000000000000000 ) ) ;
#3716=CARTESIAN_POINT ( 'NONE',  ( 3.974167765203684866, 0.7238254970431302615, -3.565825589389262085 ) ) ;
#3725=CARTESIAN_POINT ( 'NONE',  ( 4.142654963991854622, -4.070796997468703715, 6.968404583626299416E-17 ) ) ;
#3736=ORIENTED_EDGE ( 'NONE', *, *, #2154, .F. ) ;
#3779=CARTESIAN_POINT ( 'NONE',  ( 3.973110223767137850, -2.261493176400255405E-11, -3.565797985667433334 ) ) ;
#3787=ORIENTED_EDGE ( 'NONE', *, *, #8, .T. ) ;
#3788=CARTESIAN_POINT ( 'NONE',  ( 3.961545574370306966, 1.423222908132971476, -3.499999999999999556 ) ) ;
#3790=FACE_OUTER_BOUND ( 'NONE', #1235, .T. ) ;
#3806=APPLICATION_CONTEXT ( 'automotive_design' ) ;
#3851=AXIS2_PLACEMENT_3D ( 'NONE', #10404, #917, #5169 ) ;
#3904=FACE_OUTER_BOUND ( 'NONE', #7, .T. ) ;
#3909=CARTESIAN_POINT ( 'NONE',  ( 4.175572532730932096, -2.061029303918058275, -3.569807470274390493 ) ) ;
#3925=B_SPLINE_CURVE_WITH_KNOTS ( 'NONE', 3,
 ( #6076, #3909, #12410, #12274, #13433, #12340, #2874, #4123, #2947, #2808, #11446, #8135, #13365, #9173, #8067, #9380 ),
 .UNSPECIFIED., .F., .F.,
 ( 4, 3, 3, 3, 3, 4 ),
 ( -2.111273352581287704E-06, 0.000000000000000000, 3.519286887794526448E-05, 7.191842652068348909E-05, 0.0001049868727093649664, 0.0001382836236822123786 ),
 .UNSPECIFIED. ) ;
#3973=ADVANCED_FACE ( 'NONE', ( #308 ), #4671, .F. ) ;
#3976=EDGE_LOOP ( 'NONE', ( #4977, #78, #6907, #11306 ) ) ;
#3979=CARTESIAN_POINT ( 'NONE',  ( 4.071447262713888016, -2.020725942163694722, -3.499999999999999556 ) ) ;
#4000=CARTESIAN_POINT ( 'NONE',  ( 4.114405500665256454, 2.025575754679711959, 3.508400121684935424 ) ) ;
#4014=ORIENTED_EDGE ( 'NONE', *, *, #5140, .T. ) ;
#4015=AXIS2_PLACEMENT_3D ( 'NONE', #1522, #10866, #6534 ) ;
#4016=FACE_OUTER_BOUND ( 'NONE', #7604, .T. ) ;
#4049=CIRCLE ( 'NONE', #5821, 5.371010071662833063 ) ;
#4052=VERTEX_POINT ( 'NONE', #13293 ) ;
#4056=( NAMED_UNIT ( * ) PLANE_ANGLE_UNIT ( ) SI_UNIT ( $, .RADIAN. ) );
#4059=CARTESIAN_POINT ( 'NONE',  ( 4.071447262713890680, -4.041451884327386779, 0.000000000000000000 ) ) ;
#4068=CARTESIAN_POINT ( 'NONE',  ( 4.052432342741587590, 1.393590342655181891, 3.567979436357439305 ) ) ;
#4080=B_SPLINE_CURVE_WITH_KNOTS ( 'NONE', 3,
 ( #8086, #10908, #1425, #3591 ),
 .UNSPECIFIED., .F., .F.,
 ( 4, 4 ),
 ( 2.380739282773774244E-07, 0.002044882221487524104 ),
 .UNSPECIFIED. ) ;
#4089=ADVANCED_FACE ( 'NONE', ( #3904 ), #5027, .T. ) ;
#4105=CARTESIAN_POINT ( 'NONE',  ( 4.071447262713888016, 4.041451884327382338, 0.000000000000000000 ) ) ;
#4120=CARTESIAN_POINT ( 'NONE',  ( 5.599999999999999645, 4.041451884327382338, 0.000000000000000000 ) ) ;
#4123=CARTESIAN_POINT ( 'NONE',  ( 4.151274195509678577, -2.039912954708747339, -3.533232880573492274 ) ) ;
#4139=CARTESIAN_POINT ( 'NONE',  ( 4.158921784487744411, 2.089935040870091409, 3.500000000000000444 ) ) ;
#4141=CARTESIAN_POINT ( 'NONE',  ( 3.973514160553462737, -3.435084588004193140, 1.181876024140318782 ) ) ;
#4177=AXIS2_PLACEMENT_3D ( 'NONE', #11742, #2396, #12643 ) ;
#4181=CARTESIAN_POINT ( 'NONE',  ( 3.961551342853669944, 3.742715940867779700, -0.5174258321190529086 ) ) ;
#4192=CARTESIAN_POINT ( 'NONE',  ( 4.175813232069146785, 2.061359961916365613, -3.570380186727397653 ) ) ;
#4205=CARTESIAN_POINT ( 'NONE',  ( 4.175326769692857987, 4.121399112977855772, 3.964526709274768569E-16 ) ) ;
#4228=CARTESIAN_POINT ( 'NONE',  ( 4.180231891692618440, 2.049421325483208101, 3.591231015387272851 ) ) ;
#4231=ORIENTED_EDGE ( 'NONE', *, *, #2139, .F. ) ;
#4252=CARTESIAN_POINT ( 'NONE',  ( 0.000000000000000000, 0.000000000000000000, 0.000000000000000000 ) ) ;
#4265=EDGE_CURVE ( 'NONE', #8586, #7290, #10909, .T. ) ;
#4270=CARTESIAN_POINT ( 'NONE',  ( 0.02993401039713615083, 3.373851915354614928, 1.156317065392238774 ) ) ;
#4289=B_SPLINE_CURVE_WITH_KNOTS ( 'NONE', 3,
 ( #13595, #1848, #10289, #4141, #11397, #5260 ),
 .UNSPECIFIED., .F., .F.,
 ( 4, 2, 4 ),
 ( 0.000000000000000000, 0.002086519881787261485, 0.004173039763574522970 ),
 .UNSPECIFIED. ) ;
#4324=EDGE_CURVE ( 'NONE', #8026, #3586, #12888, .T. ) ;
#4330=CARTESIAN_POINT ( 'NONE',  ( 4.175326769692855322, -2.060699556488924333, 3.569236330973470928 ) ) ;
#4342=CARTESIAN_POINT ( 'NONE',  ( 4.071447262713888016, 4.041451884327382338, 0.000000000000000000 ) ) ;
#4356=EDGE_CURVE ( 'NONE', #8026, #8586, #8049, .T. ) ;
#4357=CARTESIAN_POINT ( 'NONE',  ( 0.3126073911696451990, -4.041451884327386779, -1.834154111220703958E-17 ) ) ;
#4361=CARTESIAN_POINT ( 'NONE',  ( 4.175572532730933872, -4.122058607836120103, 1.048217341165752127E-14 ) ) ;
#4386=CARTESIAN_POINT ( 'NONE',  ( 4.132952817037867987, 2.031684012687259511, -3.518979934899751694 ) ) ;
#4391=CARTESIAN_POINT ( 'NONE',  ( 4.165266963751724560, -2.049631966911991565, 3.550066703508907739 ) ) ;
#4400=PRODUCT_DEFINITION_CONTEXT ( 'detailed design', #6128, 'design' ) ;
#4406=STYLED_ITEM ( 'NONE', ( #3156 ), #7343 ) ;
#4422=CARTESIAN_POINT ( 'NONE',  ( 4.071447262713887127, 2.020725942163688504, 3.500000000000000000 ) ) ;
#4430=B_SPLINE_CURVE_WITH_KNOTS ( 'NONE', 3,
 ( #4616, #8836, #8001, #12211, #1479, #2740, #11170, #13034, #3578, #12011, #4391, #13019, #5381, #4330, #5646, #9588 ),
 .UNSPECIFIED., .F., .F.,
 ( 4, 3, 3, 3, 3, 4 ),
 ( 0.000000000000000000, 3.315506744709513341E-05, 6.608280158699547874E-05, 0.0001026520855291439131, 0.0001376952025664790686, 0.0001398064759190603148 ),
 .UNSPECIFIED. ) ;
#4456=CARTESIAN_POINT ( 'NONE',  ( 4.086262629614029862, -1.979770830881092181, -3.570936333571104626 ) ) ;
#4463=CARTESIAN_POINT ( 'NONE',  ( 0.1388410611046087539, 3.710337782248032568, 0.5735064479039790886 ) ) ;
#4471=CARTESIAN_POINT ( 'NONE',  ( 4.132952817037860882, 4.063368025374523462, 1.253603594387587993E-15 ) ) ;
#4489=EDGE_CURVE ( 'NONE', #4052, #2018, #10031, .T. ) ;
#4492=CARTESIAN_POINT ( 'NONE',  ( 7.547063560035813063E-16, -3.202582148906732762, -1.452965002680431272 ) ) ;
#4495=CARTESIAN_POINT ( 'NONE',  ( 4.158921614371307918, 4.076055977742304215, -0.05993604794450364120 ) ) ;
#4529=CONICAL_SURFACE ( 'NONE', #6318, 3.500000000000000000, 1.047197551196600296 ) ;
#4544=CARTESIAN_POINT ( 'NONE',  ( 4.180345304246197990, -2.049116244671341569, 3.591763845239312136 ) ) ;
#4553=AXIS2_PLACEMENT_3D ( 'NONE', #920, #12477, #11587 ) ;
#4571=VERTEX_POINT ( 'NONE', #4690 ) ;
#4594=CARTESIAN_POINT ( 'NONE',  ( 3.948103430090710297, -3.379418997638724331, -1.146674596026246551 ) ) ;
#4611=AXIS2_PLACEMENT_3D ( 'NONE', #9446, #11451, #10412 ) ;
#4613=CARTESIAN_POINT ( 'NONE',  ( 4.630153689607048761, 6.577590292450083844E-16, 5.371010071662833063 ) ) ;
#4616=CARTESIAN_POINT ( 'NONE',  ( 4.071447262713887127, -2.020725942163686284, 3.500000000000000444 ) ) ;
#4617=EDGE_CURVE ( 'NONE', #65, #13462, #11973, .T. ) ;
#4629=CARTESIAN_POINT ( 'NONE',  ( 3.958476099524539382, -1.406653531810738933, -3.499999999999999556 ) ) ;
#4630=EDGE_LOOP ( 'NONE', ( #11496, #11421, #3010, #12787, #7893, #9131, #10354 ) ) ;
#4637=CARTESIAN_POINT ( 'NONE',  ( 4.082498951862920222, -4.041451884327386779, 0.000000000000000000 ) ) ;
#4642=ORIENTED_EDGE ( 'NONE', *, *, #4715, .T. ) ;
#4662=CARTESIAN_POINT ( 'NONE',  ( 4.175813232069147674, 2.061359961916367833, 3.570380186727398097 ) ) ;
#4667=CARTESIAN_POINT ( 'NONE',  ( 4.050823680195224874, -2.400527758044906701, -2.978030508226146900 ) ) ;
#4671=PLANE ( 'NONE',  #13117 ) ;
#4674=CIRCLE ( 'NONE', #2236, 2.500000000000000444 ) ;
#4690=CARTESIAN_POINT ( 'NONE',  ( 45.60000000000000142, 0.000000000000000000, 2.055000000000000160 ) ) ;
#4695=VERTEX_POINT ( 'NONE', #9390 ) ;
#4697=AXIS2_PLACEMENT_3D ( 'NONE', #7929, #511, #1617 ) ;
#4698=ORIENTED_EDGE ( 'NONE', *, *, #341, .F. ) ;
#4708=CARTESIAN_POINT ( 'NONE',  ( 4.093692494532774617, -4.043567292011547742, 3.285329657490527105E-16 ) ) ;
#4715=EDGE_CURVE ( 'NONE', #12675, #1912, #5137, .T. ) ;
#4729=CARTESIAN_POINT ( 'NONE',  ( 4.175813232069148562, -2.061359961916374051, -3.570380186727397653 ) ) ;
#4733=CARTESIAN_POINT ( 'NONE',  ( 4.033901012035484790, -2.321269032827465661, -2.979444097106959788 ) ) ;
#4767=ORIENTED_EDGE ( 'NONE', *, *, #12758, .F. ) ;
#4804=CARTESIAN_POINT ( 'NONE',  ( 0.1388410611046082266, -2.351840044243035166, 2.926493552096024242 ) ) ;
#4829=ORIENTED_EDGE ( 'NONE', *, *, #12029, .T. ) ;
#4831=ORIENTED_EDGE ( 'NONE', *, *, #3251, .T. ) ;
#4837=CONICAL_SURFACE ( 'NONE', #4611, 3.500000000000000000, 1.047197551196600296 ) ;
#4839=CARTESIAN_POINT ( 'NONE',  ( 0.03027795056225670092, 0.6888063905605149584, -3.499999999999999556 ) ) ;
#4842=CARTESIAN_POINT ( 'NONE',  ( 4.124214193018072017, -4.056676826581893103, 6.968404583626299416E-17 ) ) ;
#4849=ORIENTED_EDGE ( 'NONE', *, *, #8, .F. ) ;
#4862=DIRECTION ( 'NONE',  ( 0.000000000000000000, 0.000000000000000000, 1.000000000000000000 ) ) ;
#4869=ORIENTED_EDGE ( 'NONE', *, *, #9266, .T. ) ;
#4870=EDGE_CURVE ( 'NONE', #13341, #5442, #5146, .T. ) ;
#4885=ORIENTED_EDGE ( 'NONE', *, *, #11473, .T. ) ;
#4888=CARTESIAN_POINT ( 'NONE',  ( 45.60000000000000142, 0.000000000000000000, 2.055000000000000160 ) ) ;
#4895=CARTESIAN_POINT ( 'NONE',  ( 4.071447262713887127, 2.020725942163686284, -3.499999999999999556 ) ) ;
#4949=CARTESIAN_POINT ( 'NONE',  ( 0.2174200650117537048, -2.185595227304857335, 3.214438021527933564 ) ) ;
#4977=ORIENTED_EDGE ( 'NONE', *, *, #11744, .T. ) ;
#5011=EDGE_CURVE ( 'NONE', #8586, #5283, #9412, .T. ) ;
#5027=CYLINDRICAL_SURFACE ( 'NONE', #6513, 2.500000000000000444 ) ;
#5031=FACE_OUTER_BOUND ( 'NONE', #10088, .T. ) ;
#5032=CARTESIAN_POINT ( 'NONE',  ( 45.60000000000000142, 0.000000000000000000, 0.000000000000000000 ) ) ;
#5035=( LENGTH_UNIT ( ) NAMED_UNIT ( * ) SI_UNIT ( .MILLI., .METRE. ) );
#5044=ORIENTED_EDGE ( 'NONE', *, *, #6545, .T. ) ;
#5046=ORIENTED_EDGE ( 'NONE', *, *, #7493, .T. ) ;
#5117=VERTEX_POINT ( 'NONE', #13630 ) ;
#5118=CARTESIAN_POINT ( 'NONE',  ( 3.972058292797711054, 0.6948821373584146421, 3.565770528409240026 ) ) ;
#5121=CARTESIAN_POINT ( 'NONE',  ( 4.082498951862916670, 2.020725942163688504, 3.500000000000000000 ) ) ;
#5136=DIRECTION ( 'NONE',  ( 1.000000000000000000, 0.000000000000000000, 0.000000000000000000 ) ) ;
#5137=B_SPLINE_CURVE_WITH_KNOTS ( 'NONE', 3,
 ( #6423, #12418, #3160, #5313, #11388, #12625 ),
 .UNSPECIFIED., .F., .F.,
 ( 4, 2, 4 ),
 ( 0.01308430720669670130, 0.01410661709916351952, 0.01512892699163033601 ),
 .UNSPECIFIED. ) ;
#5140=EDGE_CURVE ( 'NONE', #3165, #5335, #12539, .T. ) ;
#5146=CIRCLE ( 'NONE', #1802, 0.4999999999999978351 ) ;
#5169=DIRECTION ( 'NONE',  ( 0.000000000000000000, 0.000000000000000000, -1.000000000000000000 ) ) ;
#5186=CARTESIAN_POINT ( 'NONE',  ( 4.158806752148102248, -2.089318365061878513, 3.500000000000000000 ) ) ;
#5191=FACE_OUTER_BOUND ( 'NONE', #841, .T. ) ;
#5226=CARTESIAN_POINT ( 'NONE',  ( 4.071447262713887127, -2.020725942163686284, 3.500000000000000444 ) ) ;
#5256=ADVANCED_FACE ( 'NONE', ( #1451 ), #1381, .F. ) ;
#5260=CARTESIAN_POINT ( 'NONE',  ( 4.175813232069150338, -4.122719923832746325, 2.362127131240695889E-16 ) ) ;
#5278=CARTESIAN_POINT ( 'NONE',  ( 4.030867648404937498, 3.732851566701761659, 0.5345114293584584120 ) ) ;
#5283=VERTEX_POINT ( 'NONE', #356 ) ;
#5288=CARTESIAN_POINT ( 'NONE',  ( 4.630153689607048761, 0.000000000000000000, 0.000000000000000000 ) ) ;
#5289=CARTESIAN_POINT ( 'NONE',  ( 3.951447005078451813, 1.347150628109126558, 3.500000000000000444 ) ) ;
#5303=DIRECTION ( 'NONE',  ( 0.000000000000000000, -0.8660254037844382635, -0.5000000000000008882 ) ) ;
#5313=CARTESIAN_POINT ( 'NONE',  ( 0.1381419387168661417, -1.355287006802423644, -3.499999999999999556 ) ) ;
#5322=CARTESIAN_POINT ( 'NONE',  ( 4.052424581287827010, -2.393186648133491357, 2.990837702970496892 ) ) ;
#5332=B_SPLINE_CURVE_WITH_KNOTS ( 'NONE', 3,
 ( #8984, #7949, #13456, #4839, #2687, #6913 ),
 .UNSPECIFIED., .F., .F.,
 ( 4, 2, 4 ),
 ( 0.01103795672827925789, 0.01206113196748797960, 0.01308430720669670130 ),
 .UNSPECIFIED. ) ;
#5335=VERTEX_POINT ( 'NONE', #6595 ) ;
#5351=ORIENTED_EDGE ( 'NONE', *, *, #12174, .T. ) ;
#5370=CIRCLE ( 'NONE', #4697, 2.500000000000000444 ) ;
#5381=CARTESIAN_POINT ( 'NONE',  ( 4.175075985190095373, -2.060370777630118777, 3.568666869285566090 ) ) ;
#5395=CARTESIAN_POINT ( 'NONE',  ( 3.973110223768737015, -0.6864646529411583264, -3.565797985667475078 ) ) ;
#5407=CARTESIAN_POINT ( 'NONE',  ( 5.599999999999999645, 2.020725942163686284, -3.499999999999999556 ) ) ;
#5421=ORIENTED_EDGE ( 'NONE', *, *, #729, .T. ) ;
#5427=B_SPLINE_CURVE_WITH_KNOTS ( 'NONE', 3,
 ( #5226, #9428, #7365, #5289, #7692 ),
 .UNSPECIFIED., .F., .F.,
 ( 4, 1, 4 ),
 ( 0.000000000000000000, 0.002020725942163687470, 0.004041451884327374941 ),
 .UNSPECIFIED. ) ;
#5442=VERTEX_POINT ( 'NONE', #8369 ) ;
#5444=EDGE_CURVE ( 'NONE', #10373, #9556, #4674, .T. ) ;
#5461=CARTESIAN_POINT ( 'NONE',  ( 3.958484000407985981, -2.327740518749076948, 2.968235154689861321 ) ) ;
#5470=EDGE_CURVE ( 'NONE', #8026, #5335, #6148, .T. ) ;
#5503=CARTESIAN_POINT ( 'NONE',  ( 5.100000000000002309, 0.000000000000000000, 0.000000000000000000 ) ) ;
#5571=CARTESIAN_POINT ( 'NONE',  ( 3.972066048304772501, -3.435565134476469495, -1.180968096049828775 ) ) ;
#5600=ORIENTED_EDGE ( 'NONE', *, *, #11336, .T. ) ;
#5602=EDGE_LOOP ( 'NONE', ( #13310, #8114, #8277, #6012, #12739 ) ) ;
#5606=CARTESIAN_POINT ( 'NONE',  ( 0.3126073911696408136, 2.020725942163688060, 3.500000000000000000 ) ) ;
#5611=CARTESIAN_POINT ( 'NONE',  ( 5.599999999999999645, 2.020725942163686284, -3.499999999999999556 ) ) ;
#5638=EDGE_CURVE ( 'NONE', #10104, #3586, #5951, .T. ) ;
#5639=ADVANCED_FACE ( 'NONE', ( #10641 ), #129, .T. ) ;
#5644=B_SPLINE_CURVE_WITH_KNOTS ( 'NONE', 3,
 ( #6421, #8212, #10345, #13509, #4059 ),
 .UNSPECIFIED., .F., .F.,
 ( 4, 1, 4 ),
 ( 0.000000000000000000, 0.002020725942163690506, 0.004041451884327381013 ),
 .UNSPECIFIED. ) ;
#5646=CARTESIAN_POINT ( 'NONE',  ( 4.175572532730931208, -2.061029303918052946, 3.569807470274390493 ) ) ;
#5647=FACE_OUTER_BOUND ( 'NONE', #13076, .T. ) ;
#5666=CIRCLE ( 'NONE', #4553, 3.500000000000000000 ) ;
#5670=CARTESIAN_POINT ( 'NONE',  ( 4.030859730899086557, -1.403482646610860307, -3.500000000000000000 ) ) ;
#5672=CARTESIAN_POINT ( 'NONE',  ( 0.1388410611046073107, 2.351840044243033834, -2.926493552096022022 ) ) ;
#5680=CARTESIAN_POINT ( 'NONE',  ( 4.151274195509681242, -4.079825909417492902, 4.401844587977598791E-16 ) ) ;
#5688=ORIENTED_EDGE ( 'NONE', *, *, #7053, .T. ) ;
#5725=CARTESIAN_POINT ( 'NONE',  ( 3.973110223765528914, 0.6902454861566579281, -3.565797985667391146 ) ) ;
#5728=CARTESIAN_POINT ( 'NONE',  ( 5.599999999999999645, 3.061616997868383634E-16, -2.500000000000000444 ) ) ;
#5738=CARTESIAN_POINT ( 'NONE',  ( 3.880198502136737115, 0.7307680362927179152, -3.499999999999999556 ) ) ;
#5742=CARTESIAN_POINT ( 'NONE',  ( 45.15499999999999403, 0.000000000000000000, 0.000000000000000000 ) ) ;
#5768=EDGE_CURVE ( 'NONE', #3586, #13062, #13355, .T. ) ;
#5776=CARTESIAN_POINT ( 'NONE',  ( 4.030867648404857562, -3.732851566702167556, -0.5345114293585713217 ) ) ;
#5807=ORIENTED_EDGE ( 'NONE', *, *, #4715, .F. ) ;
#5809=CARTESIAN_POINT ( 'NONE',  ( 4.180232103119976728, 2.085387772176679366, -3.570466442734698820 ) ) ;
#5811=CARTESIAN_POINT ( 'NONE',  ( -2.919722569185572480E-15, 2.859595677584338524, -2.047034997319574945 ) ) ;
#5821=AXIS2_PLACEMENT_3D ( 'NONE', #6845, #13185, #11120 ) ;
#5828=CARTESIAN_POINT ( 'NONE',  ( 0.000000000000000000, 0.000000000000000000, 0.000000000000000000 ) ) ;
#5848=SHAPE_REPRESENTATION ( 'hex flange bolt small_iso_ISO 4162 - M5 x 40 x 16-N', ( #430 ), #9694 ) ;
#5850=ADVANCED_FACE ( 'NONE', ( #854 ), #4837, .T. ) ;
#5862=ORIENTED_EDGE ( 'NONE', *, *, #4489, .T. ) ;
#5871=CARTESIAN_POINT ( 'NONE',  ( 3.806834918298644954, 3.031088913245535199, -1.749999999999998446 ) ) ;
#5874=ORIENTED_EDGE ( 'NONE', *, *, #11247, .T. ) ;
#5878=CARTESIAN_POINT ( 'NONE',  ( 8.978549240895586059E-17, -0.3420925509381363971, 3.500000000000000444 ) ) ;
#5902=CARTESIAN_POINT ( 'NONE',  ( 0.03027795055833727364, 0.6888063905328611902, 3.500000000000000888 ) ) ;
#5915=CARTESIAN_POINT ( 'NONE',  ( 0.02993401039713673023, -2.688325911136453694, 2.343682934607768775 ) ) ;
#5925=DIRECTION ( 'NONE',  ( 0.000000000000000000, 0.000000000000000000, -1.000000000000000000 ) ) ;
#5945=CARTESIAN_POINT ( 'NONE',  ( 4.158921444904715159, -2.089933220600048713, -3.500000000000000000 ) ) ;
#5951=CIRCLE ( 'NONE', #4177, 3.500000000000000000 ) ;
#5980=ORIENTED_EDGE ( 'NONE', *, *, #4324, .T. ) ;
#5995=DIRECTION ( 'NONE',  ( -1.000000000000000000, -0.000000000000000000, -0.000000000000000000 ) ) ;
#5996=EDGE_LOOP ( 'NONE', ( #616, #2082, #11442, #2715, #2769 ) ) ;
#6012=ORIENTED_EDGE ( 'NONE', *, *, #12241, .F. ) ;
#6021=B_SPLINE_CURVE_WITH_KNOTS ( 'NONE', 3,
 ( #12727, #2283, #3335, #7297 ),
 .UNSPECIFIED., .F., .F.,
 ( 4, 4 ),
 ( 0.002080789711329271950, 0.004173039763574510827 ),
 .UNSPECIFIED. ) ;
#6053=CLOSED_SHELL ( 'NONE', ( #12944, #13604, #11518, #5639, #7976, #4089, #12854, #7212, #2924, #1640, #707, #5850, #2019, #11161, #12167, #6159, #12440, #11615, #10670, #5256, #3973, #454, #3571, #7141, #7631, #10793, #10514, #3316, #6456 ) ) ;
#6076=CARTESIAN_POINT ( 'NONE',  ( 4.175813232069148562, -2.061359961916374051, -3.570380186727397653 ) ) ;
#6108=ORIENTED_EDGE ( 'NONE', *, *, #4324, .F. ) ;
#6122=ORIENTED_EDGE ( 'NONE', *, *, #6453, .F. ) ;
#6128=APPLICATION_CONTEXT ( 'automotive_design' ) ;
#6148=B_SPLINE_CURVE_WITH_KNOTS ( 'NONE', 3,
 ( #9002, #11207, #5902, #8303, #12184, #10177 ),
 .UNSPECIFIED., .F., .F.,
 ( 4, 2, 4 ),
 ( 0.005852013098461904955, 0.006875955139453157790, 0.007899897180444410624 ),
 .UNSPECIFIED. ) ;
#6159=ADVANCED_FACE ( 'NONE', ( #5647 ), #8813, .T. ) ;
#6205=CARTESIAN_POINT ( 'NONE',  ( 4.630153689607048761, 0.000000000000000000, -5.371010071662833063 ) ) ;
#6217=DIRECTION ( 'NONE',  ( 1.000000000000000000, 0.000000000000000000, 0.000000000000000000 ) ) ;
#6222=SHAPE_REPRESENTATION_RELATIONSHIP ( 'NONE' , 'NONE' ,  #5848, #7343 ) ;
#6237=CARTESIAN_POINT ( 'NONE',  ( 4.093692494532771953, 2.021783646005768542, 3.501831996793843160 ) ) ;
#6248=ORIENTED_EDGE ( 'NONE', *, *, #7493, .F. ) ;
#6288=FACE_OUTER_BOUND ( 'NONE', #13410, .T. ) ;
#6289=CARTESIAN_POINT ( 'NONE',  ( 4.071447262713887127, 2.020725942163686284, -3.499999999999999556 ) ) ;
#6298=EDGE_LOOP ( 'NONE', ( #8861, #13282, #1771, #598 ) ) ;
#6318=AXIS2_PLACEMENT_3D ( 'NONE', #8496, #9598, #10823 ) ;
#6387=CARTESIAN_POINT ( 'NONE',  ( 4.170895651974851681, -4.109780709045220526, -1.251026243406537913E-13 ) ) ;
#6416=CARTESIAN_POINT ( 'NONE',  ( 4.082498951862918446, 2.020725942163685396, -3.500000000000001332 ) ) ;
#6421=CARTESIAN_POINT ( 'NONE',  ( 4.071447262713888016, -2.020725942163694722, -3.499999999999999556 ) ) ;
#6423=CARTESIAN_POINT ( 'NONE',  ( 0.000000000000000000, 0.000000000000000000, -3.499999999999999556 ) ) ;
#6432=CARTESIAN_POINT ( 'NONE',  ( 3.974175853610083742, -3.450041667725777472, 1.156004144284040303 ) ) ;
#6453=EDGE_CURVE ( 'NONE', #9858, #5442, #7234, .T. ) ;
#6456=ADVANCED_FACE ( 'NONE', ( #9370 ), #2271, .F. ) ;
#6470=DIRECTION ( 'NONE',  ( 0.000000000000000000, 0.000000000000000000, -1.000000000000000000 ) ) ;
#6498=CARTESIAN_POINT ( 'NONE',  ( 4.124214193018070240, 4.056676826581888662, 1.068854115921270076E-15 ) ) ;
#6501=CARTESIAN_POINT ( 'NONE',  ( 3.972066048304701891, -2.740530939476090388, 2.384802634787825504 ) ) ;
#6513=AXIS2_PLACEMENT_3D ( 'NONE', #6954, #5995, #9094 ) ;
#6519=CARTESIAN_POINT ( 'NONE',  ( 3.950241966888466738, 2.668221755853590782, 2.378504353001025695 ) ) ;
#6526=VECTOR ( 'NONE', #12710, 1000.000000000000000 ) ;
#6528=DIRECTION ( 'NONE',  ( 0.000000000000000000, 0.000000000000000000, -1.000000000000000000 ) ) ;
#6534=DIRECTION ( 'NONE',  ( 0.000000000000000000, 0.5000000000000018874, 0.8660254037844375974 ) ) ;
#6542=DIRECTION ( 'NONE',  ( -1.000000000000000000, -0.000000000000000000, -0.000000000000000000 ) ) ;
#6545=EDGE_CURVE ( 'NONE', #13432, #5283, #10234, .T. ) ;
#6555=ORIENTED_EDGE ( 'NONE', *, *, #9443, .F. ) ;
#6558=CARTESIAN_POINT ( 'NONE',  ( 4.170895651974850793, 4.109780709045216085, 3.964526709274768569E-16 ) ) ;
#6561=CARTESIAN_POINT ( 'NONE',  ( 3.973110223767137850, -2.261493176400255405E-11, -3.565797985667433334 ) ) ;
#6573=LINE ( 'NONE', #5407, #9607 ) ;
#6595=CARTESIAN_POINT ( 'NONE',  ( 0.3126073911696408136, 2.020725942163688060, 3.500000000000000000 ) ) ;
#6600=CARTESIAN_POINT ( 'NONE',  ( 5.599999999999999645, -2.020725942163694722, -3.499999999999999556 ) ) ;
#6606=CARTESIAN_POINT ( 'NONE',  ( 3.973514160553461849, 2.741076955031360285, 2.383932505289871884 ) ) ;
#6617=AXIS2_PLACEMENT_3D ( 'NONE', #9274, #11410, #1929 ) ;
#6629=CARTESIAN_POINT ( 'NONE',  ( 4.175813232069146785, 2.061359961916365613, -3.570380186727397653 ) ) ;
#6652=CARTESIAN_POINT ( 'NONE',  ( 4.086376042167606748, 4.082715877136863902, -0.07147133206917800907 ) ) ;
#6655=ORIENTED_EDGE ( 'NONE', *, *, #6545, .F. ) ;
#6669=VERTEX_POINT ( 'NONE', #6629 ) ;
#6677=CARTESIAN_POINT ( 'NONE',  ( 4.158921614371310582, -4.076055977742308656, 0.05993604794450350243 ) ) ;
#6694=DIRECTION ( 'NONE',  ( -1.000000000000000000, 0.000000000000000000, -0.000000000000000000 ) ) ;
#6710=CARTESIAN_POINT ( 'NONE',  ( 4.630153689607048761, 0.000000000000000000, 0.000000000000000000 ) ) ;
#6718=DIRECTION ( 'NONE',  ( 0.000000000000000000, -0.5000000000000012212, -0.8660254037844380415 ) ) ;
#6734=TOROIDAL_SURFACE ( 'NONE', #12027, 5.200000000000001066, 0.4999999999999978351 ) ;
#6780=CARTESIAN_POINT ( 'NONE',  ( 4.132952817037861770, -4.063368025374527015, 6.968404583626299416E-17 ) ) ;
#6804=CARTESIAN_POINT ( 'NONE',  ( 3.974175853610014908, -2.726149789692841274, -2.409821656223155806 ) ) ;
#6837=DIRECTION ( 'NONE',  ( 1.000000000000000000, 0.000000000000000000, 0.000000000000000000 ) ) ;
#6845=CARTESIAN_POINT ( 'NONE',  ( 4.630153689607048761, 0.000000000000000000, 0.000000000000000000 ) ) ;
#6872=AXIS2_PLACEMENT_3D ( 'NONE', #11801, #13659, #1144 ) ;
#6886=CONICAL_SURFACE ( 'NONE', #9099, 3.500000000000000000, 1.047197551196600296 ) ;
#6907=ORIENTED_EDGE ( 'NONE', *, *, #3563, .F. ) ;
#6913=CARTESIAN_POINT ( 'NONE',  ( 0.000000000000000000, 0.000000000000000000, -3.499999999999999556 ) ) ;
#6919=EDGE_LOOP ( 'NONE', ( #12204, #11480, #2016, #722 ) ) ;
#6921=EDGE_CURVE ( 'NONE', #2018, #4052, #5370, .T. ) ;
#6954=CARTESIAN_POINT ( 'NONE',  ( 0.000000000000000000, 0.000000000000000000, 0.000000000000000000 ) ) ;
#6967=CARTESIAN_POINT ( 'NONE',  ( 0.000000000000000000, 0.000000000000000000, 0.000000000000000000 ) ) ;
#7022=ORIENTED_EDGE ( 'NONE', *, *, #1689, .F. ) ;
#7046=CARTESIAN_POINT ( 'NONE',  ( 4.170895651974848128, 2.054890354522668439, 3.559174498016340227 ) ) ;
#7047=AXIS2_PLACEMENT_3D ( 'NONE', #2734, #11166, #5925 ) ;
#7048=CARTESIAN_POINT ( 'NONE',  ( 3.973514160553462737, 3.435084588004190476, -1.181876024140317227 ) ) ;
#7051=EDGE_CURVE ( 'NONE', #898, #9858, #3138, .T. ) ;
#7053=EDGE_CURVE ( 'NONE', #4571, #9009, #2674, .T. ) ;
#7064=CARTESIAN_POINT ( 'NONE',  ( 3.951447005078450925, -2.357513599190971032, 2.916666666666666963 ) ) ;
#7072=CARTESIAN_POINT ( 'NONE',  ( 4.071447262713887127, 2.020725942163686284, -3.499999999999999556 ) ) ;
#7080=CARTESIAN_POINT ( 'NONE',  ( 5.599999999999998757, 6.472876824008161592E-16, -5.200000000000001066 ) ) ;
#7086=CIRCLE ( 'NONE', #7534, 2.500000000000000444 ) ;
#7096=ORIENTED_EDGE ( 'NONE', *, *, #7291, .T. ) ;
#7114=ORIENTED_EDGE ( 'NONE', *, *, #4870, .F. ) ;
#7141=ADVANCED_FACE ( 'NONE', ( #11734 ), #9798, .F. ) ;
#7207=CARTESIAN_POINT ( 'NONE',  ( 4.030867648405251025, 2.329326259789668452, -2.965488570640744115 ) ) ;
#7212=ADVANCED_FACE ( 'NONE', ( #2455 ), #510, .F. ) ;
#7224=EDGE_CURVE ( 'NONE', #9006, #10405, #7799, .T. ) ;
#7234=LINE ( 'NONE', #6205, #56 ) ;
#7240=B_SPLINE_CURVE_WITH_KNOTS ( 'NONE', 3,
 ( #10457, #9362, #2997, #2928 ),
 .UNSPECIFIED., .F., .F.,
 ( 4, 4 ),
 ( 2.380739282168708963E-07, 0.002044882221487539717 ),
 .UNSPECIFIED. ) ;
#7255=ORIENTED_EDGE ( 'NONE', *, *, #11336, .F. ) ;
#7277=CARTESIAN_POINT ( 'NONE',  ( 0.000000000000000000, -3.031088913245531202, 1.750000000000006439 ) ) ;
#7286=AXIS2_PLACEMENT_3D ( 'NONE', #12938, #7640, #2364 ) ;
#7290=VERTEX_POINT ( 'NONE', #2593 ) ;
#7291=EDGE_CURVE ( 'NONE', #9858, #6669, #9725, .T. ) ;
#7297=CARTESIAN_POINT ( 'NONE',  ( 4.175813232069146785, -2.061359961916366057, 3.570380186727398542 ) ) ;
#7306=CARTESIAN_POINT ( 'NONE',  ( 4.086262629614029862, 4.082406995609985323, 0.07093633357110586124 ) ) ;
#7313=ORIENTED_EDGE ( 'NONE', *, *, #10013, .F. ) ;
#7319=FILL_AREA_STYLE ('',( #8351 ) ) ;
#7329=CARTESIAN_POINT ( 'NONE',  ( 3.880214671983734043, -0.7309020039772819999, 3.500000000000000444 ) ) ;
#7331=CARTESIAN_POINT ( 'NONE',  ( 4.630153689607048761, 6.577590292450083844E-16, 5.371010071662833063 ) ) ;
#7343=ADVANCED_BREP_SHAPE_REPRESENTATION ( '', ( #1029, #430 ), #9694 ) ;
#7358=EDGE_LOOP ( 'NONE', ( #6655, #2994, #4014, #11250, #9358 ) ) ;
#7365=CARTESIAN_POINT ( 'NONE',  ( 3.806834918298644066, 1.084202172485504434E-15, 3.500000000000000000 ) ) ;
#7372=CARTESIAN_POINT ( 'NONE',  ( 3.974175853610027342, 3.450041667725633143, -1.156004144283977908 ) ) ;
#7382=CARTESIAN_POINT ( 'NONE',  ( 4.170895651974849017, 2.054890354522707074, -3.559174498016318910 ) ) ;
#7395=AXIS2_PLACEMENT_3D ( 'NONE', #5288, #1174, #6528 ) ;
#7397=CARTESIAN_POINT ( 'NONE',  ( 3.961551342853522950, -3.742715940867789026, 0.5174258321190450260 ) ) ;
#7421=CARTESIAN_POINT ( 'NONE',  ( 4.175075985190098926, -4.120741555260250877, 2.761631486132788719E-14 ) ) ;
#7432=CARTESIAN_POINT ( 'NONE',  ( 4.175813232069147674, 2.061359961916367833, 3.570380186727398097 ) ) ;
#7445=CARTESIAN_POINT ( 'NONE',  ( 4.114405500665261783, 2.025575754679710627, -3.508400121684937645 ) ) ;
#7471=EDGE_LOOP ( 'NONE', ( #8323, #523, #6108 ) ) ;
#7473=CARTESIAN_POINT ( 'NONE',  ( 0.3126073911696407026, -2.020725942163686728, 3.500000000000000444 ) ) ;
#7493=EDGE_CURVE ( 'NONE', #6669, #13462, #1449, .T. ) ;
#7504=EDGE_LOOP ( 'NONE', ( #10712, #3365, #11928, #6122, #7096, #2856, #760 ) ) ;
#7522=EDGE_LOOP ( 'NONE', ( #5862, #2299 ) ) ;
#7534=AXIS2_PLACEMENT_3D ( 'NONE', #5742, #11883, #8850 ) ;
#7544=CARTESIAN_POINT ( 'NONE',  ( 4.158806965674306078, 1.986429158307092768, 3.559403772175832259 ) ) ;
#7570=LINE ( 'NONE', #6600, #11013 ) ;
#7574=FACE_OUTER_BOUND ( 'NONE', #3976, .T. ) ;
#7579=EDGE_CURVE ( 'NONE', #5117, #11058, #8573, .T. ) ;
#7582=DIRECTION ( 'NONE',  ( -1.000000000000000000, -0.000000000000000000, -0.000000000000000000 ) ) ;
#7597=CARTESIAN_POINT ( 'NONE',  ( 4.175813232069150338, -4.122719923832746325, 2.362127131240695889E-16 ) ) ;
#7604=EDGE_LOOP ( 'NONE', ( #11109, #4831, #5421, #5807, #6555 ) ) ;
#7606=DIRECTION ( 'NONE',  ( -1.000000000000000000, -0.000000000000000000, -0.000000000000000000 ) ) ;
#7612=CARTESIAN_POINT ( 'NONE',  ( 0.1388410611046115850, -3.710337782248037009, -0.5735064479039788665 ) ) ;
#7615=CARTESIAN_POINT ( 'NONE',  ( 4.086262629614028086, 1.979770830881088850, 3.570936333571100629 ) ) ;
#7631=ADVANCED_FACE ( 'NONE', ( #492 ), #258, .F. ) ;
#7640=DIRECTION ( 'NONE',  ( 1.000000000000000000, 0.000000000000000000, -0.000000000000000000 ) ) ;
#7651=LINE ( 'NONE', #1129, #9324 ) ;
#7681=CARTESIAN_POINT ( 'NONE',  ( 3.974175853610013132, 2.726149789692839054, 2.409821656223150033 ) ) ;
#7692=CARTESIAN_POINT ( 'NONE',  ( 4.071447262713887127, 2.020725942163688504, 3.500000000000000000 ) ) ;
#7708=AXIS2_PLACEMENT_3D ( 'NONE', #2004, #884, #5136 ) ;
#7718=DIRECTION ( 'NONE',  ( 1.000000000000000000, 0.000000000000000000, 0.000000000000000000 ) ) ;
#7729=PRODUCT_DEFINITION_FORMATION_WITH_SPECIFIED_SOURCE ( 'ANY', '', #3662, .NOT_KNOWN. ) ;
#7780=CIRCLE ( 'NONE', #1804, 5.200000000000001066 ) ;
#7799=LINE ( 'NONE', #4613, #13257 ) ;
#7821=CARTESIAN_POINT ( 'NONE',  ( 0.000000000000000000, 3.031088913245533867, 1.750000000000002887 ) ) ;
#7843=AXIS2_PLACEMENT_3D ( 'NONE', #6710, #7606, #1083 ) ;
#7848=CARTESIAN_POINT ( 'NONE',  ( 3.961551342853212532, -2.319461885623237851, -2.982574167881048677 ) ) ;
#7859=UNCERTAINTY_MEASURE_WITH_UNIT (LENGTH_MEASURE( 1.000000000000000082E-05 ), #1906, 'distance_accuracy_value', 'NONE');
#7879=CARTESIAN_POINT ( 'NONE',  ( 4.158807179406255550, 2.089320655794525639, -3.500000000000000000 ) ) ;
#7883=CARTESIAN_POINT ( 'NONE',  ( 0.000000000000000000, 0.000000000000000000, 0.000000000000000000 ) ) ;
#7893=ORIENTED_EDGE ( 'NONE', *, *, #7051, .T. ) ;
#7912=CARTESIAN_POINT ( 'NONE',  ( 4.180345304246199767, -4.135116856707399258, 0.02129519942689610257 ) ) ;
#7927=CARTESIAN_POINT ( 'NONE',  ( 4.158921614371307918, -1.986121848748762186, 3.559936047944509241 ) ) ;
#7929=CARTESIAN_POINT ( 'NONE',  ( 5.599999999999999645, 0.000000000000000000, 0.000000000000000000 ) ) ;
#7932=AXIS2_PLACEMENT_3D ( 'NONE', #2839, #11913, #9066 ) ;
#7945=EDGE_LOOP ( 'NONE', ( #5046, #1644, #2852, #880 ) ) ;
#7949=CARTESIAN_POINT ( 'NONE',  ( 0.2182387239012630320, 1.693823289460900883, -3.499999999999999112 ) ) ;
#7976=ADVANCED_FACE ( 'NONE', ( #8459, #1176 ), #9561, .T. ) ;
#7997=CARTESIAN_POINT ( 'NONE',  ( 0.000000000000000000, 0.000000000000000000, -3.499999999999999556 ) ) ;
#8001=CARTESIAN_POINT ( 'NONE',  ( 4.093692494532773729, -2.021783646005766766, 3.501831996793844493 ) ) ;
#8014=CARTESIAN_POINT ( 'NONE',  ( 0.2175679805369682140, -1.691499766289324080, 3.500000000000000000 ) ) ;
#8026=VERTEX_POINT ( 'NONE', #12664 ) ;
#8032=CARTESIAN_POINT ( 'NONE',  ( 3.806834918298644954, -3.031088913245536975, 1.750000000000000666 ) ) ;
#8049=CIRCLE ( 'NONE', #3851, 3.500000000000000000 ) ;
#8052=EDGE_CURVE ( 'NONE', #13432, #3165, #5427, .T. ) ;
#8053=PRODUCT_CONTEXT ( 'NONE', #3806, 'mechanical' ) ;
#8067=CARTESIAN_POINT ( 'NONE',  ( 4.082498951862917558, -2.020725942163694722, -3.499999999999999556 ) ) ;
#8083=ORIENTED_EDGE ( 'NONE', *, *, #7053, .F. ) ;
#8086=CARTESIAN_POINT ( 'NONE',  ( 0.3126073911695746443, -2.020725942163797750, -3.499999999999999556 ) ) ;
#8114=ORIENTED_EDGE ( 'NONE', *, *, #13481, .F. ) ;
#8135=CARTESIAN_POINT ( 'NONE',  ( 4.114405500665255566, -2.025575754679718177, -3.508400121684934980 ) ) ;
#8155=CARTESIAN_POINT ( 'NONE',  ( 4.175326769692855322, 2.060699556488906126, 3.569236330973482030 ) ) ;
#8173=CARTESIAN_POINT ( 'NONE',  ( 4.071447262713887127, -2.020725942163686284, 3.500000000000000444 ) ) ;
#8195=CARTESIAN_POINT ( 'NONE',  ( 5.100000000000002309, 6.368163355566238354E-16, -5.200000000000001066 ) ) ;
#8209=( LENGTH_UNIT ( ) NAMED_UNIT ( * ) SI_UNIT ( .MILLI., .METRE. ) );
#8212=CARTESIAN_POINT ( 'NONE',  ( 3.951447005078450925, -2.357513599190977249, -2.916666666666666519 ) ) ;
#8225=CARTESIAN_POINT ( 'NONE',  ( 4.151274195509679465, 2.039912954708742898, 3.533232880573493606 ) ) ;
#8273=ORIENTED_EDGE ( 'NONE', *, *, #4265, .T. ) ;
#8277=ORIENTED_EDGE ( 'NONE', *, *, #9059, .F. ) ;
#8287=AXIS2_PLACEMENT_3D ( 'NONE', #3710, #1694, #717 ) ;
#8292=AXIS2_PLACEMENT_3D ( 'NONE', #7883, #6837, #10149 ) ;
#8293=ORIENTED_EDGE ( 'NONE', *, *, #5011, .T. ) ;
#8296=EDGE_CURVE ( 'NONE', #4695, #13432, #142, .T. ) ;
#8303=CARTESIAN_POINT ( 'NONE',  ( 0.1397371499203167444, 1.362866705341264195, 3.499999999999999556 ) ) ;
#8315=( BOUNDED_SURFACE ( )  B_SPLINE_SURFACE ( 3, 2, ( 
 ( #7615, #7544, #4228 ),
 ( #3260, #8651, #1094 ),
 ( #2273, #6519, #7681 ),
 ( #9753, #11755, #274 ),
 ( #11627, #5278, #75 ),
 ( #6652, #4495, #2207 ) ),
 .UNSPECIFIED., .F., .F., .F. ) 
 B_SPLINE_SURFACE_WITH_KNOTS ( ( 4, 2, 4 ),
 ( 3, 3 ),
 ( 0.01651999345535505245, 0.01858032176739834312, 0.02064065007944163727 ),
 ( 0.000000000000000000, 1.000000000000000000 ),
 .UNSPECIFIED. ) 
 GEOMETRIC_REPRESENTATION_ITEM ( )  RATIONAL_B_SPLINE_SURFACE ( (
 ( 1.000000000000000000, 0.8047781103519393575, 1.000000000000000000),
 ( 1.000000000000000000, 0.8123785825604844524, 1.000000000000000000),
 ( 1.000000000000000000, 0.8190671539787625077, 1.000000000000000000),
 ( 1.000000000000000000, 0.8192352254835536529, 1.000000000000000000),
 ( 1.000000000000000000, 0.8126129677211098024, 1.000000000000000000),
 ( 1.000000000000000000, 0.8047712537969730073, 1.000000000000000000) ) ) 
 REPRESENTATION_ITEM ( '' )  SURFACE ( )  );
#8323=ORIENTED_EDGE ( 'NONE', *, *, #5470, .T. ) ;
#8351=FILL_AREA_STYLE_COLOUR ( '', #2629 ) ;
#8360=CARTESIAN_POINT ( 'NONE',  ( 4.180345472528542494, 2.086001522971430600, 3.570468649087212398 ) ) ;
#8361=CARTESIAN_POINT ( 'NONE',  ( 4.071447262713887127, 2.020725942163688504, 3.500000000000000000 ) ) ;
#8369=CARTESIAN_POINT ( 'NONE',  ( 4.630153689607048761, 0.000000000000000000, -5.371010071662833063 ) ) ;
#8404=CARTESIAN_POINT ( 'NONE',  ( 4.055492966679587141, 3.795017426214561063, -0.5629142681441071661 ) ) ;
#8410=ORIENTED_EDGE ( 'NONE', *, *, #3251, .F. ) ;
#8415=CARTESIAN_POINT ( 'NONE',  ( 4.175075985190094485, 2.060370777630093464, -3.568666869285578080 ) ) ;
#8428=CARTESIAN_POINT ( 'NONE',  ( 4.175572532730932096, 4.122058607836116551, 1.170198429493232648E-15 ) ) ;
#8430=CARTESIAN_POINT ( 'NONE',  ( 4.180231891692622881, -4.134807952925578789, -0.02076457676760693274 ) ) ;
#8459=FACE_BOUND ( 'NONE', #7522, .T. ) ;
#8470=DIRECTION ( 'NONE',  ( 0.000000000000000000, 0.000000000000000000, -1.000000000000000000 ) ) ;
#8480=CARTESIAN_POINT ( 'NONE',  ( 4.151274195509685683, 2.039912954708744230, -3.533232880573500267 ) ) ;
#8488=CARTESIAN_POINT ( 'NONE',  ( 0.3126073911696427010, 4.041451884327382338, -6.521455134176256610E-17 ) ) ;
#8496=CARTESIAN_POINT ( 'NONE',  ( 0.000000000000000000, 0.000000000000000000, 0.000000000000000000 ) ) ;
#8500=AXIS2_PLACEMENT_3D ( 'NONE', #4252, #984, #8470 ) ;
#8514=CONICAL_SURFACE ( 'NONE', #10925, 2.055000000000000160, 0.7853981633974400633 ) ;
#8527=DIRECTION ( 'NONE',  ( -0.000000000000000000, 0.000000000000000000, -1.000000000000000000 ) ) ;
#8546=CARTESIAN_POINT ( 'NONE',  ( 4.124214193018076458, 2.028338413290941222, -3.513185186763556622 ) ) ;
#8552=B_SPLINE_CURVE_WITH_KNOTS ( 'NONE', 3,
 ( #5606, #12778, #9815, #13048 ),
 .UNSPECIFIED., .F., .F.,
 ( 4, 4 ),
 ( 2.380739282167303683E-07, 0.002044882221487525839 ),
 .UNSPECIFIED. ) ;
#8573=B_SPLINE_CURVE_WITH_KNOTS ( 'NONE', 3,
 ( #12058, #2439, #8950, #6606, #237, #4662 ),
 .UNSPECIFIED., .F., .F.,
 ( 4, 2, 4 ),
 ( 0.000000000000000000, 0.002086519881787259317, 0.004173039763574518633 ),
 .UNSPECIFIED. ) ;
#8586=VERTEX_POINT ( 'NONE', #7277 ) ;
#8608=CARTESIAN_POINT ( 'NONE',  ( 0.1217565302851100623, 3.710888496608919507, -0.5725525826504660465 ) ) ;
#8611=CARTESIAN_POINT ( 'NONE',  ( 4.158413352280813768, 2.044871626972823986, -3.541821552872968404 ) ) ;
#8620=CARTESIAN_POINT ( 'NONE',  ( 0.2174200650117547873, 3.876582599186211731, 0.2855619784720684895 ) ) ;
#8629=CARTESIAN_POINT ( 'NONE',  ( 0.3126073911695746443, -2.020725942163797750, -3.499999999999999556 ) ) ;
#8641=EDGE_CURVE ( 'NONE', #9009, #4571, #649, .T. ) ;
#8643=EDGE_CURVE ( 'NONE', #9556, #10373, #7086, .T. ) ;
#8651=CARTESIAN_POINT ( 'NONE',  ( 4.033901012036116285, 2.321269032827693035, 2.979444097106929146 ) ) ;
#8677=VERTEX_POINT ( 'NONE', #4357 ) ;
#8678=FACE_OUTER_BOUND ( 'NONE', #9918, .T. ) ;
#8697=CARTESIAN_POINT ( 'NONE',  ( 4.086262629614032527, -4.082406995609991540, -0.07093633357110748494 ) ) ;
#8703=EDGE_CURVE ( 'NONE', #5335, #3586, #8552, .T. ) ;
#8707=B_SPLINE_CURVE_WITH_KNOTS ( 'NONE', 3,
 ( #2103, #8608, #1191, #12679 ),
 .UNSPECIFIED., .F., .F.,
 ( 4, 4 ),
 ( 2.380739282169052541E-07, 0.002044882221487534079 ),
 .UNSPECIFIED. ) ;
#8714=DIRECTION ( 'NONE',  ( -1.000000000000000000, -0.000000000000000000, -0.000000000000000000 ) ) ;
#8729=ORIENTED_EDGE ( 'NONE', *, *, #8641, .T. ) ;
#8762=CARTESIAN_POINT ( 'NONE',  ( 4.175813232069147674, 2.061359961916367833, 3.570380186727398097 ) ) ;
#8813=CONICAL_SURFACE ( 'NONE', #9262, 3.500000000000000000, 1.047197551196600296 ) ;
#8833=EDGE_CURVE ( 'NONE', #6669, #5117, #121, .T. ) ;
#8836=CARTESIAN_POINT ( 'NONE',  ( 4.082498951862918446, -2.020725942163685840, 3.500000000000002220 ) ) ;
#8849=CARTESIAN_POINT ( 'NONE',  ( 0.02993401039713550899, 2.688325911136453250, -2.343682934607766111 ) ) ;
#8850=DIRECTION ( 'NONE',  ( 0.000000000000000000, 0.000000000000000000, 1.000000000000000000 ) ) ;
#8853=CARTESIAN_POINT ( 'NONE',  ( 0.000000000000000000, -3.031088913245534755, -1.750000000000001332 ) ) ;
#8859=AXIS2_PLACEMENT_3D ( 'NONE', #10961, #6694, #3504 ) ;
#8861=ORIENTED_EDGE ( 'NONE', *, *, #5444, .T. ) ;
#8885=CARTESIAN_POINT ( 'NONE',  ( 4.158806965674307854, -1.986429158307096321, -3.559403772175836256 ) ) ;
#8890=CARTESIAN_POINT ( 'NONE',  ( 4.175813232069148562, -2.061359961916374051, -3.570380186727397653 ) ) ;
#8896=CARTESIAN_POINT ( 'NONE',  ( 5.599999999999999645, 2.020725942163688504, 3.500000000000000000 ) ) ;
#8921=CARTESIAN_POINT ( 'NONE',  ( 4.050536630291688311, 2.401306687817038821, -2.976670123173768001 ) ) ;
#8926=CARTESIAN_POINT ( 'NONE',  ( 4.114405500665258231, -4.051151509359434577, 3.301207616706364010E-16 ) ) ;
#8948=EDGE_LOOP ( 'NONE', ( #1372, #10871, #10922, #1455, #7255 ) ) ;
#8950=CARTESIAN_POINT ( 'NONE',  ( 3.972709601346592123, 3.429395227388311262, 1.191688283765307332 ) ) ;
#8961=ORIENTED_EDGE ( 'NONE', *, *, #4265, .F. ) ;
#8984=CARTESIAN_POINT ( 'NONE',  ( 0.3126073911696399255, 2.020725942163686284, -3.499999999999999556 ) ) ;
#9002=CARTESIAN_POINT ( 'NONE',  ( 0.000000000000000000, 3.755786496842903495E-16, 3.500000000000000000 ) ) ;
#9006=VERTEX_POINT ( 'NONE', #1920 ) ;
#9009=VERTEX_POINT ( 'NONE', #10562 ) ;
#9028=CARTESIAN_POINT ( 'NONE',  ( 5.599999999999999645, -4.041451884327386779, 0.000000000000000000 ) ) ;
#9031=CARTESIAN_POINT ( 'NONE',  ( 4.050480423730738799, 1.376911654797411400, -3.567926555162023394 ) ) ;
#9044=CARTESIAN_POINT ( 'NONE',  ( 3.878104551856474735, -0.7018542299754126912, -3.499999999999999556 ) ) ;
#9050=CARTESIAN_POINT ( 'NONE',  ( 4.175813232069148562, 4.122719923832741884, -2.765695189283172261E-17 ) ) ;
#9059=EDGE_CURVE ( 'NONE', #11058, #9006, #942, .T. ) ;
#9066=DIRECTION ( 'NONE',  ( 0.000000000000000000, 0.000000000000000000, 1.000000000000000000 ) ) ;
#9076=CARTESIAN_POINT ( 'NONE',  ( 45.15499999999999403, 0.000000000000000000, 0.000000000000000000 ) ) ;
#9085=CARTESIAN_POINT ( 'NONE',  ( 5.599999999999998757, 0.000000000000000000, 5.200000000000001066 ) ) ;
#9094=DIRECTION ( 'NONE',  ( 0.000000000000000000, 0.000000000000000000, 1.000000000000000000 ) ) ;
#9099=AXIS2_PLACEMENT_3D ( 'NONE', #6967, #12145, #11938 ) ;
#9118=CARTESIAN_POINT ( 'NONE',  ( 3.958491816111018746, 1.406739583089935186, 3.500000000000000000 ) ) ;
#9131=ORIENTED_EDGE ( 'NONE', *, *, #6453, .T. ) ;
#9162=CARTESIAN_POINT ( 'NONE',  ( 0.3126073911696407026, -2.020725942163686728, 3.500000000000000444 ) ) ;
#9173=CARTESIAN_POINT ( 'NONE',  ( 4.093692494532771953, -2.021783646005774759, -3.501831996793842716 ) ) ;
#9187=CARTESIAN_POINT ( 'NONE',  ( 5.599999999999999645, -2.020725942163694722, -3.499999999999999556 ) ) ;
#9244=SURFACE_STYLE_FILL_AREA ( #7319 ) ;
#9256=DIRECTION ( 'NONE',  ( -0.000000000000000000, 0.8660254037844383745, 0.5000000000000004441 ) ) ;
#9262=AXIS2_PLACEMENT_3D ( 'NONE', #12949, #7718, #2515 ) ;
#9266=EDGE_CURVE ( 'NONE', #7290, #8677, #2765, .T. ) ;
#9274=CARTESIAN_POINT ( 'NONE',  ( 5.599999999999998757, 0.000000000000000000, 0.000000000000000000 ) ) ;
#9287=ORIENTED_EDGE ( 'NONE', *, *, #12136, .T. ) ;
#9324=VECTOR ( 'NONE', #2376, 1000.000000000000000 ) ;
#9328=PLANE ( 'NONE',  #13421 ) ;
#9330=CARTESIAN_POINT ( 'NONE',  ( 4.132952817037859994, 2.031684012687258623, 3.518979934899746809 ) ) ;
#9358=ORIENTED_EDGE ( 'NONE', *, *, #12029, .F. ) ;
#9362=CARTESIAN_POINT ( 'NONE',  ( 0.1217565302851118803, -3.710888496608922171, 0.5725525826504672677 ) ) ;
#9370=FACE_OUTER_BOUND ( 'NONE', #7945, .T. ) ;
#9380=CARTESIAN_POINT ( 'NONE',  ( 4.071447262713888016, -2.020725942163694722, -3.499999999999999556 ) ) ;
#9390=CARTESIAN_POINT ( 'NONE',  ( 4.071447262713890680, -4.041451884327386779, 0.000000000000000000 ) ) ;
#9399=CARTESIAN_POINT ( 'NONE',  ( 4.033906725095553369, -1.419670120619691334, 3.500000000000000444 ) ) ;
#9412=B_SPLINE_CURVE_WITH_KNOTS ( 'NONE', 3,
 ( #2797, #1744, #5915, #4804, #4949, #9162 ),
 .UNSPECIFIED., .F., .F.,
 ( 4, 2, 4 ),
 ( 0.002044882221487539717, 0.003063384235218500652, 0.004081886248949461587 ),
 .UNSPECIFIED. ) ;
#9420=CARTESIAN_POINT ( 'NONE',  ( 4.071447262713887127, 2.020725942163688504, 3.500000000000000000 ) ) ;
#9428=CARTESIAN_POINT ( 'NONE',  ( 3.951447005078450037, -1.347150628109123893, 3.500000000000000888 ) ) ;
#9443=EDGE_CURVE ( 'NONE', #9655, #12675, #5332, .T. ) ;
#9446=CARTESIAN_POINT ( 'NONE',  ( 0.000000000000000000, 0.000000000000000000, 0.000000000000000000 ) ) ;
#9508=DIRECTION ( 'NONE',  ( 0.000000000000000000, 0.5000000000000007772, -0.8660254037844381525 ) ) ;
#9543=CARTESIAN_POINT ( 'NONE',  ( 3.951447005078450925, 2.357513599190970144, 2.916666666666667407 ) ) ;
#9556=VERTEX_POINT ( 'NONE', #10638 ) ;
#9561=PLANE ( 'NONE',  #10418 ) ;
#9568=CARTESIAN_POINT ( 'NONE',  ( 5.599999999999999645, 2.020725942163688504, 3.500000000000000000 ) ) ;
#9588=CARTESIAN_POINT ( 'NONE',  ( 4.175813232069146785, -2.061359961916366057, 3.570380186727398542 ) ) ;
#9590=CARTESIAN_POINT ( 'NONE',  ( -1.959187206999195895E-15, 3.202582148906728765, 1.452965002680430828 ) ) ;
#9594=ORIENTED_EDGE ( 'NONE', *, *, #2481, .F. ) ;
#9596=CARTESIAN_POINT ( 'NONE',  ( 4.142654963991853734, 4.070796997468700162, 1.458723597913840680E-15 ) ) ;
#9598=DIRECTION ( 'NONE',  ( 1.000000000000000000, 0.000000000000000000, 0.000000000000000000 ) ) ;
#9607=VECTOR ( 'NONE', #1224, 1000.000000000000000 ) ;
#9650=CARTESIAN_POINT ( 'NONE',  ( 0.000000000000000000, 0.000000000000000000, 2.500000000000000444 ) ) ;
#9655=VERTEX_POINT ( 'NONE', #2258 ) ;
#9658=UNCERTAINTY_MEASURE_WITH_UNIT (LENGTH_MEASURE( 1.000000000000000082E-05 ), #5035, 'distance_accuracy_value', 'NONE');
#9663=CARTESIAN_POINT ( 'NONE',  ( 4.086376042167606748, -1.979461949354202499, 3.571471332069183990 ) ) ;
#9694=( GEOMETRIC_REPRESENTATION_CONTEXT ( 3 ) GLOBAL_UNCERTAINTY_ASSIGNED_CONTEXT ( ( #9658 ) ) GLOBAL_UNIT_ASSIGNED_CONTEXT ( ( #5035, #13581, #12344 ) ) REPRESENTATION_CONTEXT ( 'NONE', 'WORKASPACE' ) );
#9695=( NAMED_UNIT ( * ) SI_UNIT ( $, .STERADIAN. ) SOLID_ANGLE_UNIT ( ) );
#9697=AXIS2_PLACEMENT_3D ( 'NONE', #710, #6217, #11235 ) ;
#9725=B_SPLINE_CURVE_WITH_KNOTS ( 'NONE', 3,
 ( #9799, #5725, #9031, #11936 ),
 .UNSPECIFIED., .F., .F.,
 ( 4, 4 ),
 ( 0.002080789711329296236, 0.004173039763574516031 ),
 .UNSPECIFIED. ) ;
#9729=CARTESIAN_POINT ( 'NONE',  ( 4.158413352280809328, 4.089743253945647972, 1.634918261399485461E-15 ) ) ;
#9745=ORIENTED_EDGE ( 'NONE', *, *, #3430, .F. ) ;
#9753=CARTESIAN_POINT ( 'NONE',  ( 3.878096787214571517, 3.381939201670116191, 1.142309474598433461 ) ) ;
#9760=ORIENTED_EDGE ( 'NONE', *, *, #11225, .T. ) ;
#9776=ORIENTED_EDGE ( 'NONE', *, *, #5011, .F. ) ;
#9780=CARTESIAN_POINT ( 'NONE',  ( 4.086376042167608524, -4.082715877136868343, 0.07147133206917789805 ) ) ;
#9785=CARTESIAN_POINT ( 'NONE',  ( 5.599999999999998757, 0.000000000000000000, 0.000000000000000000 ) ) ;
#9793=UNCERTAINTY_MEASURE_WITH_UNIT (LENGTH_MEASURE( 1.000000000000000082E-05 ), #8209, 'distance_accuracy_value', 'NONE');
#9798=( BOUNDED_SURFACE ( )  B_SPLINE_SURFACE ( 3, 2, ( 
 ( #8697, #2323, #8430 ),
 ( #7397, #184, #55 ),
 ( #12760, #11608, #6432 ),
 ( #2120, #2252, #6501 ),
 ( #5461, #1070, #5322 ),
 ( #9663, #7927, #4544 ) ),
 .UNSPECIFIED., .F., .F., .F. ) 
 B_SPLINE_SURFACE_WITH_KNOTS ( ( 4, 2, 4 ),
 ( 3, 3 ),
 ( 0.01651999345535504551, 0.01858032176739835006, 0.02064065007944165114 ),
 ( 0.000000000000000000, 1.000000000000000000 ),
 .UNSPECIFIED. ) 
 GEOMETRIC_REPRESENTATION_ITEM ( )  RATIONAL_B_SPLINE_SURFACE ( (
 ( 1.000000000000000000, 0.8047781103519391355, 1.000000000000000000),
 ( 1.000000000000000000, 0.8123785825613523137, 1.000000000000000000),
 ( 1.000000000000000000, 0.8190671539776074317, 1.000000000000000000),
 ( 1.000000000000000000, 0.8192352254847047321, 1.000000000000000000),
 ( 1.000000000000000000, 0.8126129677202470480, 1.000000000000000000),
 ( 1.000000000000000000, 0.8047712537969722302, 1.000000000000000000) ) ) 
 REPRESENTATION_ITEM ( '' )  SURFACE ( )  );
#9799=CARTESIAN_POINT ( 'NONE',  ( 3.973110223767137850, -2.261493176400255405E-11, -3.565797985667433334 ) ) ;
#9815=CARTESIAN_POINT ( 'NONE',  ( -1.935715396507168721E-15, 2.686816014504566752, 2.346298152288372130 ) ) ;
#9850=B_SPLINE_CURVE_WITH_KNOTS ( 'NONE', 3,
 ( #4342, #12892, #10698, #11731, #2321, #6498, #4471, #9596, #13657, #9729, #1212, #6558, #1142, #4205, #8428, #10493 ),
 .UNSPECIFIED., .F., .F.,
 ( 4, 3, 3, 3, 3, 4 ),
 ( 0.000000000000000000, 3.315506744709155554E-05, 6.608280158698769959E-05, 0.0001026520855291340739, 0.0001376952025664813454, 0.0001398064759190616429 ),
 .UNSPECIFIED. ) ;
#9858=VERTEX_POINT ( 'NONE', #3779 ) ;
#9864=FACE_OUTER_BOUND ( 'NONE', #7471, .T. ) ;
#9874=CARTESIAN_POINT ( 'NONE',  ( 0.000000000000000000, 3.755786496842903495E-16, 3.500000000000000000 ) ) ;
#9906=CONICAL_SURFACE ( 'NONE', #9697, 3.500000000000000000, 1.047197551196600296 ) ;
#9913=CARTESIAN_POINT ( 'NONE',  ( 4.175813232069150338, -4.122719923832746325, 2.362127131240695889E-16 ) ) ;
#9918=EDGE_LOOP ( 'NONE', ( #5688, #12098, #10301, #13480 ) ) ;
#9939=CARTESIAN_POINT ( 'NONE',  ( 4.086375874528100027, -2.103253014742892280, -3.499999999999999556 ) ) ;
#9988=B_SPLINE_CURVE_WITH_KNOTS ( 'NONE', 3,
 ( #12224, #5811, #8849, #5672, #2825, #10008 ),
 .UNSPECIFIED., .F., .F.,
 ( 4, 2, 4 ),
 ( 0.002044882221487534079, 0.003063384235218496315, 0.004081886248949458985 ),
 .UNSPECIFIED. ) ;
#10004=CARTESIAN_POINT ( 'NONE',  ( 4.180345136606690382, -2.085999704580137060, -3.570468642550115312 ) ) ;
#10005=B_SPLINE_CURVE_WITH_KNOTS ( 'NONE', 3,
 ( #7072, #2920, #11352, #1874, #10312 ),
 .UNSPECIFIED., .F., .F.,
 ( 4, 1, 4 ),
 ( 0.000000000000000000, 0.002020725942163690506, 0.004041451884327381013 ),
 .UNSPECIFIED. ) ;
#10008=CARTESIAN_POINT ( 'NONE',  ( 0.3126073911696399255, 2.020725942163686284, -3.499999999999999556 ) ) ;
#10013=EDGE_CURVE ( 'NONE', #12709, #4695, #5644, .T. ) ;
#10031=CIRCLE ( 'NONE', #8287, 2.500000000000000444 ) ;
#10064=CARTESIAN_POINT ( 'NONE',  ( 3.951447005078450037, 2.357513599190969256, -2.916666666666667407 ) ) ;
#10078=CARTESIAN_POINT ( 'NONE',  ( 4.050823680195224874, 3.779313952391379239, -0.5899027668435166127 ) ) ;
#10088=EDGE_LOOP ( 'NONE', ( #4829, #13296, #8293 ) ) ;
#10104=VERTEX_POINT ( 'NONE', #10686 ) ;
#10112=VECTOR ( 'NONE', #2453, 1000.000000000000000 ) ;
#10125=LINE ( 'NONE', #4888, #1278 ) ;
#10134=CIRCLE ( 'NONE', #6617, 5.200000000000001066 ) ;
#10145=CARTESIAN_POINT ( 'NONE',  ( 4.052416734886645777, -1.393505408945131308, -3.567979131523694836 ) ) ;
#10149=DIRECTION ( 'NONE',  ( 0.000000000000000000, 0.000000000000000000, -1.000000000000000000 ) ) ;
#10177=CARTESIAN_POINT ( 'NONE',  ( 0.3126073911696408136, 2.020725942163688060, 3.500000000000000000 ) ) ;
#10202=DIRECTION ( 'NONE',  ( -0.7071067811865533459, 0.000000000000000000, 0.7071067811865416886 ) ) ;
#10234=LINE ( 'NONE', #1722, #2692 ) ;
#10253=AXIS2_PLACEMENT_3D ( 'NONE', #3009, #1964, #3145 ) ;
#10286=CARTESIAN_POINT ( 'NONE',  ( 4.086376210449952140, 2.103254844323300343, 3.500000000000000000 ) ) ;
#10289=CARTESIAN_POINT ( 'NONE',  ( 3.972709601346592123, -2.746729940827190575, 2.374099244652734697 ) ) ;
#10293=AXIS2_PLACEMENT_3D ( 'NONE', #4120, #5303, #9508 ) ;
#10301=ORIENTED_EDGE ( 'NONE', *, *, #5444, .F. ) ;
#10312=CARTESIAN_POINT ( 'NONE',  ( 4.071447262713888016, -2.020725942163694722, -3.499999999999999556 ) ) ;
#10340=DIRECTION ( 'NONE',  ( 0.000000000000000000, 0.000000000000000000, 1.000000000000000000 ) ) ;
#10345=CARTESIAN_POINT ( 'NONE',  ( 3.806834918298644954, -3.031088913245541416, -1.749999999999998890 ) ) ;
#10354=ORIENTED_EDGE ( 'NONE', *, *, #11929, .T. ) ;
#10355=CARTESIAN_POINT ( 'NONE',  ( 4.180231680468789790, -2.085385483809538698, 3.570466434508605680 ) ) ;
#10360=AXIS2_PLACEMENT_3D ( 'NONE', #296, #1791, #364 ) ;
#10373=VERTEX_POINT ( 'NONE', #13192 ) ;
#10383=ORIENTED_EDGE ( 'NONE', *, *, #8703, .F. ) ;
#10401=DIRECTION ( 'NONE',  ( 0.3420201433256622736, 0.000000000000000000, -0.9396926207859106484 ) ) ;
#10404=CARTESIAN_POINT ( 'NONE',  ( 0.000000000000000000, 0.000000000000000000, 0.000000000000000000 ) ) ;
#10405=VERTEX_POINT ( 'NONE', #7331 ) ;
#10406=PLANE ( 'NONE',  #10293 ) ;
#10412=DIRECTION ( 'NONE',  ( 0.000000000000000000, 0.000000000000000000, -1.000000000000000000 ) ) ;
#10418=AXIS2_PLACEMENT_3D ( 'NONE', #84, #1038, #8527 ) ;
#10426=FACE_OUTER_BOUND ( 'NONE', #5602, .T. ) ;
#10431=CARTESIAN_POINT ( 'NONE',  ( 5.100000000000002309, 0.000000000000000000, 0.000000000000000000 ) ) ;
#10457=CARTESIAN_POINT ( 'NONE',  ( 0.3126073911696451990, -4.041451884327386779, -1.834154111220703958E-17 ) ) ;
#10478=DIRECTION ( 'NONE',  ( -0.7071067811865533459, 8.659560562354861368E-17, -0.7071067811865416886 ) ) ;
#10493=CARTESIAN_POINT ( 'NONE',  ( 4.175813232069148562, 4.122719923832741884, -2.765695189283172261E-17 ) ) ;
#10495=CARTESIAN_POINT ( 'NONE',  ( 4.142654963991853734, 2.035398498734346973, 3.525413613457309747 ) ) ;
#10514=ADVANCED_FACE ( 'NONE', ( #12222 ), #1054, .F. ) ;
#10541=FACE_OUTER_BOUND ( 'NONE', #2753, .T. ) ;
#10562=CARTESIAN_POINT ( 'NONE',  ( 45.60000000000000142, 2.789133085058097101E-16, -2.055000000000000160 ) ) ;
#10585=CARTESIAN_POINT ( 'NONE',  ( 4.158413352280810216, -4.089743253945651524, 4.401844587977598791E-16 ) ) ;
#10638=CARTESIAN_POINT ( 'NONE',  ( 45.15499999999999403, 3.061616997868383634E-16, -2.500000000000000444 ) ) ;
#10641=FACE_OUTER_BOUND ( 'NONE', #6298, .T. ) ;
#10660=EDGE_LOOP ( 'NONE', ( #12855, #5600, #13553 ) ) ;
#10669=CARTESIAN_POINT ( 'NONE',  ( 3.973110223768738791, 0.6864646529411682074, 3.565797985667475967 ) ) ;
#10670=ADVANCED_FACE ( 'NONE', ( #3655 ), #9328, .F. ) ;
#10686=CARTESIAN_POINT ( 'NONE',  ( 0.000000000000000000, 3.031088913245533423, -1.750000000000004885 ) ) ;
#10698=CARTESIAN_POINT ( 'NONE',  ( 4.093692494532771953, 4.043567292011543302, -5.737475420082528345E-17 ) ) ;
#10712=ORIENTED_EDGE ( 'NONE', *, *, #9059, .T. ) ;
#10753=CARTESIAN_POINT ( 'NONE',  ( 0.000000000000000000, 3.031088913245533867, 1.750000000000002887 ) ) ;
#10759=FACE_OUTER_BOUND ( 'NONE', #11181, .T. ) ;
#10793=ADVANCED_FACE ( 'NONE', ( #10426 ), #12455, .F. ) ;
#10823=DIRECTION ( 'NONE',  ( 0.000000000000000000, 0.000000000000000000, -1.000000000000000000 ) ) ;
#10866=DIRECTION ( 'NONE',  ( 0.000000000000000000, 0.8660254037844375974, -0.5000000000000018874 ) ) ;
#10871=ORIENTED_EDGE ( 'NONE', *, *, #4617, .T. ) ;
#10894=EDGE_CURVE ( 'NONE', #65, #5117, #9850, .T. ) ;
#10904=CARTESIAN_POINT ( 'NONE',  ( 3.950233766685291137, 0.7256672287179410930, -3.499999999999844125 ) ) ;
#10908=CARTESIAN_POINT ( 'NONE',  ( 0.1217565302851044418, -2.351289329882175760, -2.927447417349501535 ) ) ;
#10909=CIRCLE ( 'NONE', #8500, 3.500000000000000000 ) ;
#10922=ORIENTED_EDGE ( 'NONE', *, *, #11911, .T. ) ;
#10925=AXIS2_PLACEMENT_3D ( 'NONE', #5032, #13435, #10340 ) ;
#10961=CARTESIAN_POINT ( 'NONE',  ( 45.60000000000000142, 0.000000000000000000, 0.000000000000000000 ) ) ;
#10990=DIRECTION ( 'NONE',  ( 0.000000000000000000, 0.000000000000000000, 1.000000000000000000 ) ) ;
#11009=CARTESIAN_POINT ( 'NONE',  ( 3.878096787214417862, -3.381939201670079331, -1.142309474598505181 ) ) ;
#11013=VECTOR ( 'NONE', #3482, 1000.000000000000000 ) ;
#11041=CARTESIAN_POINT ( 'NONE',  ( 3.972073812946708582, -0.6951863858492246528, -3.565770933504603057 ) ) ;
#11043=CARTESIAN_POINT ( 'NONE',  ( 0.1381419387119174058, -1.355287006778759018, 3.500000000000000888 ) ) ;
#11045=CARTESIAN_POINT ( 'NONE',  ( 4.175813232069146785, 2.061359961916365613, -3.570380186727397653 ) ) ;
#11053=ORIENTED_EDGE ( 'NONE', *, *, #11473, .F. ) ;
#11058=VERTEX_POINT ( 'NONE', #8762 ) ;
#11069=EDGE_CURVE ( 'NONE', #4695, #8677, #13027, .T. ) ;
#11078=CARTESIAN_POINT ( 'NONE',  ( 0.3126073911696427010, 4.041451884327382338, -6.521455134176256610E-17 ) ) ;
#11088=EDGE_CURVE ( 'NONE', #898, #12709, #3925, .T. ) ;
#11105=CARTESIAN_POINT ( 'NONE',  ( 4.071447262713888016, 4.041451884327382338, 0.000000000000000000 ) ) ;
#11109=ORIENTED_EDGE ( 'NONE', *, *, #11911, .F. ) ;
#11120=DIRECTION ( 'NONE',  ( 0.000000000000000000, 0.000000000000000000, 1.000000000000000000 ) ) ;
#11161=ADVANCED_FACE ( 'NONE', ( #5031 ), #9906, .T. ) ;
#11166=DIRECTION ( 'NONE',  ( 0.000000000000000000, -1.000000000000000000, 0.000000000000000000 ) ) ;
#11170=CARTESIAN_POINT ( 'NONE',  ( 4.132952817037866211, -2.031684012687259511, 3.518979934899751250 ) ) ;
#11181=EDGE_LOOP ( 'NONE', ( #5351, #12549, #4642 ) ) ;
#11207=CARTESIAN_POINT ( 'NONE',  ( 1.677125235563514178E-16, 0.3423821193476823121, 3.500000000000000444 ) ) ;
#11225=EDGE_CURVE ( 'NONE', #13443, #10405, #12337, .T. ) ;
#11232=CIRCLE ( 'NONE', #10360, 3.500000000000000000 ) ;
#11235=DIRECTION ( 'NONE',  ( 0.000000000000000000, 0.000000000000000000, -1.000000000000000000 ) ) ;
#11247=EDGE_CURVE ( 'NONE', #4571, #10373, #10125, .T. ) ;
#11250=ORIENTED_EDGE ( 'NONE', *, *, #5470, .F. ) ;
#11256=CARTESIAN_POINT ( 'NONE',  ( 4.175075985190095373, 2.060370777630105898, 3.568666869285574972 ) ) ;
#11274=CARTESIAN_POINT ( 'NONE',  ( 4.158921614371307030, 1.986121848748763741, -3.559936047944503912 ) ) ;
#11275=CARTESIAN_POINT ( 'NONE',  ( 3.951447005078453589, -3.704664227300103807, 0.5833333333333329263 ) ) ;
#11306=ORIENTED_EDGE ( 'NONE', *, *, #11225, .F. ) ;
#11320=CARTESIAN_POINT ( 'NONE',  ( 3.948095570617042860, 0.6965071952218068185, 3.500000000000155875 ) ) ;
#11331=MECHANICAL_DESIGN_GEOMETRIC_PRESENTATION_REPRESENTATION('',(#70),#2268);
#11336=EDGE_CURVE ( 'NONE', #13062, #10104, #8707, .T. ) ;
#11350=TOROIDAL_SURFACE ( 'NONE', #12663, 5.200000000000001066, 0.4999999999999978351 ) ;
#11352=CARTESIAN_POINT ( 'NONE',  ( 3.806834918298644066, -4.553649124439118623E-15, -3.499999999999999556 ) ) ;
#11369=DIRECTION ( 'NONE',  ( 0.000000000000000000, -1.224646799147353947E-16, 1.000000000000000000 ) ) ;
#11370=CONICAL_SURFACE ( 'NONE', #8292, 3.500000000000000000, 1.047197551196600296 ) ;
#11376=EDGE_LOOP ( 'NONE', ( #13362, #7313, #50, #9594 ) ) ;
#11388=CARTESIAN_POINT ( 'NONE',  ( 0.2175679805410235534, -1.691499766303381058, -3.499999999999999556 ) ) ;
#11394=CARTESIAN_POINT ( 'NONE',  ( 4.086262418390198548, -2.102635014057361751, 3.500000000000000444 ) ) ;
#11397=CARTESIAN_POINT ( 'NONE',  ( 4.050823680195226650, -3.779313952391382792, 0.5899027668435167238 ) ) ;
#11410=DIRECTION ( 'NONE',  ( -1.000000000000000000, -0.000000000000000000, -0.000000000000000000 ) ) ;
#11421=ORIENTED_EDGE ( 'NONE', *, *, #13481, .T. ) ;
#11442=ORIENTED_EDGE ( 'NONE', *, *, #11069, .T. ) ;
#11446=CARTESIAN_POINT ( 'NONE',  ( 4.124214193018069352, -2.028338413290947440, -3.513185186763551737 ) ) ;
#11451=DIRECTION ( 'NONE',  ( 1.000000000000000000, 0.000000000000000000, 0.000000000000000000 ) ) ;
#11468=DIRECTION ( 'NONE',  ( -1.000000000000000000, -0.000000000000000000, -0.000000000000000000 ) ) ;
#11473=EDGE_CURVE ( 'NONE', #12675, #10104, #11232, .T. ) ;
#11480=ORIENTED_EDGE ( 'NONE', *, *, #7579, .F. ) ;
#11496=ORIENTED_EDGE ( 'NONE', *, *, #7224, .F. ) ;
#11514=CARTESIAN_POINT ( 'NONE',  ( 4.158806965674307854, 4.075748668183981849, 0.05940377217583739378 ) ) ;
#11518=ADVANCED_FACE ( 'NONE', ( #8678 ), #608, .T. ) ;
#11581=CARTESIAN_POINT ( 'NONE',  ( 3.878096787214415642, 2.680238624820947990, -2.357690525401575421 ) ) ;
#11587=DIRECTION ( 'NONE',  ( 0.000000000000000000, 0.000000000000000000, -1.000000000000000000 ) ) ;
#11608=CARTESIAN_POINT ( 'NONE',  ( 3.950241966888158540, -3.393956070638132871, 1.121495646998118545 ) ) ;
#11615=ADVANCED_FACE ( 'NONE', ( #4016 ), #811, .F. ) ;
#11627=CARTESIAN_POINT ( 'NONE',  ( 3.958484000407329617, 3.734437307742037415, 0.5317648453100634054 ) ) ;
#11641=CARTESIAN_POINT ( 'NONE',  ( 4.630153689607048761, 0.000000000000000000, 0.000000000000000000 ) ) ;
#11718=AXIS2_PLACEMENT_3D ( 'NONE', #3322, #8714, #11814 ) ;
#11731=CARTESIAN_POINT ( 'NONE',  ( 4.104070371397481765, 4.047367226856738220, -5.737475420082528345E-17 ) ) ;
#11734=FACE_OUTER_BOUND ( 'NONE', #13396, .T. ) ;
#11742=CARTESIAN_POINT ( 'NONE',  ( 0.000000000000000000, 0.000000000000000000, 0.000000000000000000 ) ) ;
#11744=EDGE_CURVE ( 'NONE', #13443, #13341, #10134, .T. ) ;
#11748=VECTOR ( 'NONE', #3070, 1000.000000000000000 ) ;
#11755=CARTESIAN_POINT ( 'NONE',  ( 3.948103430090398991, 3.379418997638670596, 1.146674596026254322 ) ) ;
#11801=CARTESIAN_POINT ( 'NONE',  ( 45.60000000000000142, 0.000000000000000000, 0.000000000000000000 ) ) ;
#11814=DIRECTION ( 'NONE',  ( 0.000000000000000000, 0.000000000000000000, 1.000000000000000000 ) ) ;
#11825=ORIENTED_EDGE ( 'NONE', *, *, #5638, .F. ) ;
#11850=EDGE_CURVE ( 'NONE', #3165, #65, #1914, .T. ) ;
#11880=CARTESIAN_POINT ( 'NONE',  ( 4.071447262713888016, 4.041451884327382338, 0.000000000000000000 ) ) ;
#11883=DIRECTION ( 'NONE',  ( -1.000000000000000000, -0.000000000000000000, -0.000000000000000000 ) ) ;
#11897=PRODUCT_DEFINITION ( 'UNKNOWN', '', #7729, #4400 ) ;
#11910=PLANE ( 'NONE',  #7286 ) ;
#11911=EDGE_CURVE ( 'NONE', #13462, #9655, #6573, .T. ) ;
#11913=DIRECTION ( 'NONE',  ( -1.000000000000000000, -0.000000000000000000, -0.000000000000000000 ) ) ;
#11928=ORIENTED_EDGE ( 'NONE', *, *, #3563, .T. ) ;
#11929=EDGE_CURVE ( 'NONE', #5442, #10405, #315, .T. ) ;
#11936=CARTESIAN_POINT ( 'NONE',  ( 4.175813232069146785, 2.061359961916365613, -3.570380186727397653 ) ) ;
#11938=DIRECTION ( 'NONE',  ( 0.000000000000000000, 0.000000000000000000, -1.000000000000000000 ) ) ;
#11964=EDGE_CURVE ( 'NONE', #65, #13062, #2200, .T. ) ;
#11973=B_SPLINE_CURVE_WITH_KNOTS ( 'NONE', 3,
 ( #11105, #1623, #5871, #10064, #4895 ),
 .UNSPECIFIED., .F., .F.,
 ( 4, 1, 4 ),
 ( 5.337851785822274535E-20, 0.002020725942163691374, 0.004041451884327382747 ),
 .UNSPECIFIED. ) ;
#12011=CARTESIAN_POINT ( 'NONE',  ( 4.158413352280813768, -2.044871626972823542, 3.541821552872969736 ) ) ;
#12027=AXIS2_PLACEMENT_3D ( 'NONE', #10431, #11468, #3173 ) ;
#12029=EDGE_CURVE ( 'NONE', #5283, #8026, #12152, .T. ) ;
#12058=CARTESIAN_POINT ( 'NONE',  ( 4.175813232069148562, 4.122719923832741884, -2.765695189283172261E-17 ) ) ;
#12098=ORIENTED_EDGE ( 'NONE', *, *, #12758, .T. ) ;
#12128=CARTESIAN_POINT ( 'NONE',  ( 3.972709601346593455, -3.429395227388317036, -1.191688283765307110 ) ) ;
#12136=EDGE_CURVE ( 'NONE', #10104, #9655, #9988, .T. ) ;
#12145=DIRECTION ( 'NONE',  ( 1.000000000000000000, 0.000000000000000000, 0.000000000000000000 ) ) ;
#12152=B_SPLINE_CURVE_WITH_KNOTS ( 'NONE', 3,
 ( #7473, #8014, #11043, #393, #5878, #9874 ),
 .UNSPECIFIED., .F., .F.,
 ( 4, 2, 4 ),
 ( 0.003805861006858101119, 0.004828937052660003254, 0.005852013098461904955 ),
 .UNSPECIFIED. ) ;
#12167=ADVANCED_FACE ( 'NONE', ( #3790 ), #11370, .T. ) ;
#12174=EDGE_CURVE ( 'NONE', #1912, #7290, #4080, .T. ) ;
#12184=CARTESIAN_POINT ( 'NONE',  ( 0.2182387239031248760, 1.693823289467350168, 3.500000000000000000 ) ) ;
#12204=ORIENTED_EDGE ( 'NONE', *, *, #12241, .T. ) ;
#12211=CARTESIAN_POINT ( 'NONE',  ( 4.104070371397484429, -2.023683613428364669, 3.505122836902509587 ) ) ;
#12222=FACE_OUTER_BOUND ( 'NONE', #634, .T. ) ;
#12224=CARTESIAN_POINT ( 'NONE',  ( 0.000000000000000000, 3.031088913245533423, -1.750000000000004885 ) ) ;
#12241=EDGE_CURVE ( 'NONE', #3165, #11058, #432, .T. ) ;
#12264=DIRECTION ( 'NONE',  ( -0.000000000000000000, 1.000000000000000000, 1.224646799147353207E-16 ) ) ;
#12274=CARTESIAN_POINT ( 'NONE',  ( 4.175075985190096262, -2.060370777630117889, -3.568666869285569643 ) ) ;
#12291=CARTESIAN_POINT ( 'NONE',  ( 3.950250160040163383, -0.7258013381021514165, 3.499999999999845013 ) ) ;
#12337=CIRCLE ( 'NONE', #7047, 0.4999999999999978351 ) ;
#12339=ORIENTED_EDGE ( 'NONE', *, *, #9443, .T. ) ;
#12340=CARTESIAN_POINT ( 'NONE',  ( 4.165266963751721008, -2.049631966911996006, -3.550066703508900190 ) ) ;
#12344=( NAMED_UNIT ( * ) SI_UNIT ( $, .STERADIAN. ) SOLID_ANGLE_UNIT ( ) );
#12409=ORIENTED_EDGE ( 'NONE', *, *, #2327, .F. ) ;
#12410=CARTESIAN_POINT ( 'NONE',  ( 4.175326769692856210, -2.060699556488920337, -3.569236330973475813 ) ) ;
#12418=CARTESIAN_POINT ( 'NONE',  ( -2.134523027080836115E-16, -0.3420925509533478404, -3.499999999999999112 ) ) ;
#12440=ADVANCED_FACE ( 'NONE', ( #10759 ), #4529, .T. ) ;
#12443=CARTESIAN_POINT ( 'NONE',  ( 3.958484000407829217, 2.327740518749080056, -2.968235154689852440 ) ) ;
#12455=( BOUNDED_SURFACE ( )  B_SPLINE_SURFACE ( 3, 2, ( 
 ( #11394, #5186, #10355 ),
 ( #866, #9399, #652 ),
 ( #7329, #12291, #13592 ),
 ( #1773, #11320, #5118 ),
 ( #9118, #13520, #4068 ),
 ( #10286, #4139, #8360 ) ),
 .UNSPECIFIED., .F., .F., .F. ) 
 B_SPLINE_SURFACE_WITH_KNOTS ( ( 4, 2, 4 ),
 ( 3, 3 ),
 ( 0.01651732063679904258, 0.01857756227444016389, 0.02063780391208128520 ),
 ( 0.000000000000000000, 1.000000000000000000 ),
 .UNSPECIFIED. ) 
 GEOMETRIC_REPRESENTATION_ITEM ( )  RATIONAL_B_SPLINE_SURFACE ( (
 ( 1.000000000000000000, 0.8047781231227483234, 1.000000000000000000),
 ( 1.000000000000000000, 0.8123782108664983070, 1.000000000000000000),
 ( 1.000000000000000000, 0.8190665102133478648, 1.000000000000000000),
 ( 1.000000000000000000, 0.8192358432844011329, 1.000000000000000000),
 ( 1.000000000000000000, 0.8126132624435309371, 1.000000000000000000),
 ( 1.000000000000000000, 0.8047712436238877443, 1.000000000000000000) ) ) 
 REPRESENTATION_ITEM ( '' )  SURFACE ( )  );
#12477=DIRECTION ( 'NONE',  ( 1.000000000000000000, 0.000000000000000000, -0.000000000000000000 ) ) ;
#12481=LINE ( 'NONE', #13367, #3212 ) ;
#12497=CARTESIAN_POINT ( 'NONE',  ( 4.165266963751721896, 2.049631966911991565, 3.550066703508901078 ) ) ;
#12539=LINE ( 'NONE', #9568, #11748 ) ;
#12549=ORIENTED_EDGE ( 'NONE', *, *, #341, .T. ) ;
#12593=EDGE_LOOP ( 'NONE', ( #2198, #1506, #5044, #9776, #4849 ) ) ;
#12609=CARTESIAN_POINT ( 'NONE',  ( 3.880206590543185730, 3.396506438958505125, -1.117078279489029935 ) ) ;
#12620=CARTESIAN_POINT ( 'NONE',  ( 4.142654963991859951, 2.035398498734348305, -3.525413613457315076 ) ) ;
#12625=CARTESIAN_POINT ( 'NONE',  ( 0.3126073911695746443, -2.020725942163797750, -3.499999999999999556 ) ) ;
#12630=VECTOR ( 'NONE', #3561, 1000.000000000000000 ) ;
#12631=EDGE_LOOP ( 'NONE', ( #8083, #2892 ) ) ;
#12643=DIRECTION ( 'NONE',  ( 0.000000000000000000, 0.000000000000000000, -1.000000000000000000 ) ) ;
#12663=AXIS2_PLACEMENT_3D ( 'NONE', #5503, #6542, #1053 ) ;
#12664=CARTESIAN_POINT ( 'NONE',  ( 0.000000000000000000, 3.755786496842903495E-16, 3.500000000000000000 ) ) ;
#12675=VERTEX_POINT ( 'NONE', #7997 ) ;
#12679=CARTESIAN_POINT ( 'NONE',  ( 0.000000000000000000, 3.031088913245533423, -1.750000000000004885 ) ) ;
#12709=VERTEX_POINT ( 'NONE', #3979 ) ;
#12710=DIRECTION ( 'NONE',  ( -1.000000000000000000, -0.000000000000000000, -0.000000000000000000 ) ) ;
#12727=CARTESIAN_POINT ( 'NONE',  ( 3.973110223767137850, 2.263269463293572928E-11, 3.565797985667434222 ) ) ;
#12739=ORIENTED_EDGE ( 'NONE', *, *, #8052, .F. ) ;
#12755=ORIENTED_EDGE ( 'NONE', *, *, #8643, .F. ) ;
#12756=ORIENTED_EDGE ( 'NONE', *, *, #11744, .F. ) ;
#12758=EDGE_CURVE ( 'NONE', #9009, #9556, #12481, .T. ) ;
#12760=CARTESIAN_POINT ( 'NONE',  ( 3.880206590543186618, -3.396506438958517116, 1.117078279489015502 ) ) ;
#12770=DIRECTION ( 'NONE',  ( -1.000000000000000000, -0.000000000000000000, -0.000000000000000000 ) ) ;
#12778=CARTESIAN_POINT ( 'NONE',  ( 0.1217565302851095904, 2.351289329882149559, 2.927447417349536618 ) ) ;
#12785=ORIENTED_EDGE ( 'NONE', *, *, #8296, .F. ) ;
#12787=ORIENTED_EDGE ( 'NONE', *, *, #2481, .T. ) ;
#12810=CARTESIAN_POINT ( 'NONE',  ( 4.165266963751723672, 2.049631966911992009, -3.550066703508905963 ) ) ;
#12843=CARTESIAN_POINT ( 'NONE',  ( 3.951447005078451813, 3.704664227300101143, 0.5833333333333334814 ) ) ;
#12854=ADVANCED_FACE ( 'NONE', ( #6288 ), #8514, .T. ) ;
#12855=ORIENTED_EDGE ( 'NONE', *, *, #5768, .T. ) ;
#12875=CARTESIAN_POINT ( 'NONE',  ( 3.880206590543187950, -2.665671387532591474, -2.382921720510934538 ) ) ;
#12888=CIRCLE ( 'NONE', #10253, 3.500000000000000000 ) ;
#12892=CARTESIAN_POINT ( 'NONE',  ( 4.082498951862917558, 4.041451884327382338, 3.558567857214853949E-17 ) ) ;
#12916=CARTESIAN_POINT ( 'NONE',  ( 4.175326769692858875, -4.121399112977860213, 3.677815466159040336E-14 ) ) ;
#12938=CARTESIAN_POINT ( 'NONE',  ( 0.000000000000000000, 4.041451884327382338, 0.000000000000000000 ) ) ;
#12944=ADVANCED_FACE ( 'NONE', ( #7574 ), #11350, .T. ) ;
#12949=CARTESIAN_POINT ( 'NONE',  ( 0.000000000000000000, 0.000000000000000000, 0.000000000000000000 ) ) ;
#13019=CARTESIAN_POINT ( 'NONE',  ( 4.170895651974849905, -2.054890354522598273, 3.559174498016383748 ) ) ;
#13027=LINE ( 'NONE', #9028, #10112 ) ;
#13034=CARTESIAN_POINT ( 'NONE',  ( 4.142654963991859063, -2.035398498734348305, 3.525413613457315076 ) ) ;
#13048=CARTESIAN_POINT ( 'NONE',  ( 0.000000000000000000, 3.031088913245533867, 1.750000000000002887 ) ) ;
#13050=CARTESIAN_POINT ( 'NONE',  ( 0.02993401039713891598, -3.373851915354620257, -1.156317065392238774 ) ) ;
#13062=VERTEX_POINT ( 'NONE', #11078 ) ;
#13076=EDGE_LOOP ( 'NONE', ( #9287, #12339, #4885 ) ) ;
#13117=AXIS2_PLACEMENT_3D ( 'NONE', #8896, #3295, #2245 ) ;
#13125=CARTESIAN_POINT ( 'NONE',  ( 4.104070371397483541, -4.047367226856742661, 3.293285021600925981E-16 ) ) ;
#13136=B_SPLINE_CURVE_WITH_KNOTS ( 'NONE', 3,
 ( #3192, #4361, #12916, #7421, #6387, #2142, #10585, #5680, #3725, #6780, #4842, #8926, #13125, #4708, #4637, #13253 ),
 .UNSPECIFIED., .F., .F.,
 ( 4, 3, 3, 3, 3, 4 ),
 ( -2.111273352579798197E-06, 0.000000000000000000, 3.519286887794736512E-05, 7.191842652068568460E-05, 0.0001049868727093669315, 0.0001382836236822145742 ),
 .UNSPECIFIED. ) ;
#13143=PRODUCT_DEFINITION_SHAPE ( 'NONE', 'NONE',  #11897 ) ;
#13175=CARTESIAN_POINT ( 'NONE',  ( 4.086262841041386373, 2.102637316508698451, -3.499999999999999556 ) ) ;
#13185=DIRECTION ( 'NONE',  ( -1.000000000000000000, -0.000000000000000000, -0.000000000000000000 ) ) ;
#13192=CARTESIAN_POINT ( 'NONE',  ( 45.15499999999999403, 0.000000000000000000, 2.500000000000000444 ) ) ;
#13253=CARTESIAN_POINT ( 'NONE',  ( 4.071447262713890680, -4.041451884327386779, 0.000000000000000000 ) ) ;
#13257=VECTOR ( 'NONE', #1615, 1000.000000000000114 ) ;
#13282=ORIENTED_EDGE ( 'NONE', *, *, #2327, .T. ) ;
#13293=CARTESIAN_POINT ( 'NONE',  ( 5.599999999999999645, 0.000000000000000000, 2.500000000000000444 ) ) ;
#13296=ORIENTED_EDGE ( 'NONE', *, *, #4356, .T. ) ;
#13310=ORIENTED_EDGE ( 'NONE', *, *, #2139, .T. ) ;
#13341=VERTEX_POINT ( 'NONE', #7080 ) ;
#13355=B_SPLINE_CURVE_WITH_KNOTS ( 'NONE', 3,
 ( #10753, #9590, #4270, #4463, #8620, #8488 ),
 .UNSPECIFIED., .F., .F.,
 ( 4, 2, 4 ),
 ( 0.002044882221487525839, 0.003063384235218491979, 0.004081886248949458118 ),
 .UNSPECIFIED. ) ;
#13362=ORIENTED_EDGE ( 'NONE', *, *, #3430, .T. ) ;
#13365=CARTESIAN_POINT ( 'NONE',  ( 4.104070371397480876, -2.023683613428371775, -3.505122836902506922 ) ) ;
#13367=CARTESIAN_POINT ( 'NONE',  ( 45.60000000000000142, 2.516649172247811061E-16, -2.055000000000000160 ) ) ;
#13396=EDGE_LOOP ( 'NONE', ( #4231, #12785, #9745, #7022 ) ) ;
#13410=EDGE_LOOP ( 'NONE', ( #4767, #8729, #5874, #12755 ) ) ;
#13413=ORIENTED_EDGE ( 'NONE', *, *, #11964, .T. ) ;
#13421=AXIS2_PLACEMENT_3D ( 'NONE', #9187, #9256, #13448 ) ;
#13432=VERTEX_POINT ( 'NONE', #764 ) ;
#13433=CARTESIAN_POINT ( 'NONE',  ( 4.170895651974849017, -2.054890354522642237, -3.559174498016357102 ) ) ;
#13435=DIRECTION ( 'NONE',  ( -1.000000000000000000, -0.000000000000000000, -0.000000000000000000 ) ) ;
#13443=VERTEX_POINT ( 'NONE', #9085 ) ;
#13448=DIRECTION ( 'NONE',  ( 0.000000000000000000, -0.5000000000000004441, 0.8660254037844383745 ) ) ;
#13456=CARTESIAN_POINT ( 'NONE',  ( 0.1397371499201710277, 1.362866705336852169, -3.500000000000000000 ) ) ;
#13462=VERTEX_POINT ( 'NONE', #3131 ) ;
#13480=ORIENTED_EDGE ( 'NONE', *, *, #11247, .F. ) ;
#13481=EDGE_CURVE ( 'NONE', #9006, #2696, #6021, .T. ) ;
#13509=CARTESIAN_POINT ( 'NONE',  ( 3.951447005078454477, -3.704664227300105583, -0.5833333333333333703 ) ) ;
#13520=CARTESIAN_POINT ( 'NONE',  ( 4.030875481282487627, 1.403567514399325367, 3.500000000000000000 ) ) ;
#13553=ORIENTED_EDGE ( 'NONE', *, *, #5638, .T. ) ;
#13581=( NAMED_UNIT ( * ) PLANE_ANGLE_UNIT ( ) SI_UNIT ( $, .RADIAN. ) );
#13592=CARTESIAN_POINT ( 'NONE',  ( 3.974183935050568106, -0.7239581970520293508, 3.565826011443134824 ) ) ;
#13595=CARTESIAN_POINT ( 'NONE',  ( 4.175813232069146785, -2.061359961916366057, 3.570380186727398542 ) ) ;
#13604=ADVANCED_FACE ( 'NONE', ( #1037 ), #736, .T. ) ;
#13630=CARTESIAN_POINT ( 'NONE',  ( 4.175813232069148562, 4.122719923832741884, -2.765695189283172261E-17 ) ) ;
#13632=CARTESIAN_POINT ( 'NONE',  ( 4.180231891692620216, 4.134807952925572572, 0.02076457676760539231 ) ) ;
#13657=CARTESIAN_POINT ( 'NONE',  ( 4.151274195509680354, 4.079825909417489349, 1.184320329358001550E-15 ) ) ;
#13659=DIRECTION ( 'NONE',  ( -1.000000000000000000, -0.000000000000000000, -0.000000000000000000 ) ) ;
#13706=COLOUR_RGB('Black',0.12,0.14,0.17);
#13707=FILL_AREA_STYLE_COLOUR('',#13706);
#13708=FILL_AREA_STYLE('',(#13707));
#13709=SURFACE_STYLE_FILL_AREA(#13708);
#13710=SURFACE_SIDE_STYLE('',(#13709));
#13711=SURFACE_STYLE_USAGE(.BOTH.,#13710);
#13712=PRESENTATION_STYLE_ASSIGNMENT((#13711));
ENDSEC;
END-ISO-10303-21;
